ISO-10303-21;
HEADER;
/* Generated by software containing ST-Developer
 * from STEP Tools, Inc. (www.steptools.com) 
 */

FILE_DESCRIPTION(
/* description */ ('Independent manual two-gate roller-track escapement for nominal30mm d
iameter20mm wide feed rollers. Opposed gates are driven by native capt
ured pin-slot loops with positive curved-slot travel stops at\X\B116de
g. Repeated gate/pin/washer/clip instances, adapted native common bear
ing families, full retaining lips and rotating polymer grip. External 
workpieces, gravity feeder/incline and mount anchors outside assembly.
 No powered-feed compatibility, impact, capacity, safety, force, wear 
or life rating.'),
/* implementation_level */ '2;1');

FILE_NAME(
/* name */ 'Socket head cap screw M4x10.step',
/* time_stamp */ '2026-11-08T18:43:23-08:00',
/* author */ (''),
/* organization */ (''),
/* preprocessor_version */ 'ST-DEVELOPER v20.2',
/* originating_system */ 'Autodesk Translation Framework v15.17.0.0',
/* authorisation */ '');

FILE_SCHEMA (('AUTOMOTIVE_DESIGN { 1 0 10303 214 3 1 1 }'));
ENDSEC;

DATA;
#10=MECHANICAL_DESIGN_GEOMETRIC_PRESENTATION_REPRESENTATION('',(#473),#19863);
#116=CONICAL_SURFACE('',#7146,1.5,0.785398163397449);
#125=B_SPLINE_SURFACE_WITH_KNOTS('',3,3,((#18814,#18815,#18816,#18817,#18818,
#18819,#18820,#18821,#18822,#18823,#18824,#18825,#18826,#18827,#18828,#18829,
#18830,#18831,#18832,#18833,#18834,#18835,#18836,#18837,#18838,#18839,#18840,
#18841,#18842,#18843,#18844,#18845,#18846,#18847,#18848,#18849,#18850,#18851,
#18852,#18853,#18854,#18855,#18856,#18857,#18858,#18859,#18860,#18861,#18862,
#18863,#18864,#18865,#18866,#18867,#18868,#18869,#18870,#18871,#18872,#18873,
#18874,#18875,#18876,#18877,#18878,#18879,#18880,#18881,#18882,#18883,#18884,
#18885,#18886,#18887,#18888,#18889,#18890,#18891,#18892,#18893,#18894,#18895,
#18896,#18897,#18898,#18899,#18900,#18901),(#18902,#18903,#18904,#18905,
#18906,#18907,#18908,#18909,#18910,#18911,#18912,#18913,#18914,#18915,#18916,
#18917,#18918,#18919,#18920,#18921,#18922,#18923,#18924,#18925,#18926,#18927,
#18928,#18929,#18930,#18931,#18932,#18933,#18934,#18935,#18936,#18937,#18938,
#18939,#18940,#18941,#18942,#18943,#18944,#18945,#18946,#18947,#18948,#18949,
#18950,#18951,#18952,#18953,#18954,#18955,#18956,#18957,#18958,#18959,#18960,
#18961,#18962,#18963,#18964,#18965,#18966,#18967,#18968,#18969,#18970,#18971,
#18972,#18973,#18974,#18975,#18976,#18977,#18978,#18979,#18980,#18981,#18982,
#18983,#18984,#18985,#18986,#18987,#18988,#18989),(#18990,#18991,#18992,
#18993,#18994,#18995,#18996,#18997,#18998,#18999,#19000,#19001,#19002,#19003,
#19004,#19005,#19006,#19007,#19008,#19009,#19010,#19011,#19012,#19013,#19014,
#19015,#19016,#19017,#19018,#19019,#19020,#19021,#19022,#19023,#19024,#19025,
#19026,#19027,#19028,#19029,#19030,#19031,#19032,#19033,#19034,#19035,#19036,
#19037,#19038,#19039,#19040,#19041,#19042,#19043,#19044,#19045,#19046,#19047,
#19048,#19049,#19050,#19051,#19052,#19053,#19054,#19055,#19056,#19057,#19058,
#19059,#19060,#19061,#19062,#19063,#19064,#19065,#19066,#19067,#19068,#19069,
#19070,#19071,#19072,#19073,#19074,#19075,#19076,#19077),(#19078,#19079,
#19080,#19081,#19082,#19083,#19084,#19085,#19086,#19087,#19088,#19089,#19090,
#19091,#19092,#19093,#19094,#19095,#19096,#19097,#19098,#19099,#19100,#19101,
#19102,#19103,#19104,#19105,#19106,#19107,#19108,#19109,#19110,#19111,#19112,
#19113,#19114,#19115,#19116,#19117,#19118,#19119,#19120,#19121,#19122,#19123,
#19124,#19125,#19126,#19127,#19128,#19129,#19130,#19131,#19132,#19133,#19134,
#19135,#19136,#19137,#19138,#19139,#19140,#19141,#19142,#19143,#19144,#19145,
#19146,#19147,#19148,#19149,#19150,#19151,#19152,#19153,#19154,#19155,#19156,
#19157,#19158,#19159,#19160,#19161,#19162,#19163,#19164,#19165)),
 .UNSPECIFIED.,.F.,.F.,.F.,(4,4),(4,1,1,1,1,1,1,1,1,1,1,1,1,1,1,1,1,1,1,
1,1,1,1,1,1,1,1,1,1,1,1,1,1,1,1,1,1,1,1,1,1,1,1,1,1,1,1,1,1,1,1,1,1,1,1,
1,1,1,1,1,1,1,1,1,1,1,1,1,1,1,1,1,1,1,1,1,1,1,1,1,1,1,1,1,1,4),(0.,0.0460148164544132),
(11.6154215191106,12.6127583869031,13.6100952546957,14.6074321224883,15.6047689902808,
16.6021058580734,17.599442725866,18.5967795936585,19.5941164614511,20.5914533292437,
21.5887901970362,22.5861270648288,23.5834639326213,24.5808008004139,25.5781376682065,
26.575474535999,27.5728114037916,28.5701482715842,29.5674851393767,30.5648220071693,
31.5621588749619,32.5594957427544,33.556832610547,34.5541694783396,35.5515063461321,
36.5488432139247,37.5461800817173,38.5435169495098,39.5408538173024,40.538190685095,
41.5355275528875,42.5328644206801,43.5302012884726,44.5275381562652,45.5248750240578,
46.5222118918503,47.5195487596429,48.5168856274355,49.514222495228,50.5115593630206,
51.5088962308132,52.5062330986057,53.5035699663983,54.5009068341909,55.4982437019834,
56.495580569776,57.4929174375686,58.4902543053611,59.4875911731537,60.4849280409463,
61.4822649087388,62.4796017765314,63.4769386443239,64.4742755121165,65.4716123799091,
66.4689492477016,67.4662861154942,68.4636229832868,69.4609598510793,70.4582967188719,
71.4556335866645,72.452970454457,73.4503073222496,74.4476441900422,75.4449810578347,
76.4423179256273,77.4396547934198,78.4369916612124,79.434328529005,80.4316653967976,
81.4290022645901,82.4263391323827,83.4236760001752,84.4210128679678,85.4183497357604,
86.4156866035529,87.4130234713455,88.4103603391381,89.4076972069306,90.4050340747232,
91.4023709425158,92.3997078103083,93.3970446781009,94.3943815458935,95.391718413686,
96.3890552814786),.UNSPECIFIED.);
#126=B_SPLINE_SURFACE_WITH_KNOTS('',3,3,((#19288,#19289,#19290,#19291,#19292,
#19293,#19294,#19295,#19296,#19297,#19298,#19299,#19300,#19301,#19302,#19303,
#19304,#19305,#19306,#19307,#19308,#19309,#19310,#19311,#19312,#19313,#19314,
#19315,#19316,#19317,#19318,#19319,#19320,#19321,#19322,#19323,#19324,#19325,
#19326,#19327,#19328,#19329,#19330,#19331,#19332,#19333,#19334,#19335,#19336,
#19337,#19338,#19339,#19340,#19341,#19342,#19343,#19344,#19345,#19346,#19347,
#19348,#19349,#19350,#19351,#19352,#19353,#19354,#19355,#19356,#19357,#19358,
#19359,#19360,#19361,#19362,#19363,#19364,#19365,#19366,#19367,#19368,#19369,
#19370,#19371,#19372,#19373,#19374,#19375,#19376,#19377),(#19378,#19379,
#19380,#19381,#19382,#19383,#19384,#19385,#19386,#19387,#19388,#19389,#19390,
#19391,#19392,#19393,#19394,#19395,#19396,#19397,#19398,#19399,#19400,#19401,
#19402,#19403,#19404,#19405,#19406,#19407,#19408,#19409,#19410,#19411,#19412,
#19413,#19414,#19415,#19416,#19417,#19418,#19419,#19420,#19421,#19422,#19423,
#19424,#19425,#19426,#19427,#19428,#19429,#19430,#19431,#19432,#19433,#19434,
#19435,#19436,#19437,#19438,#19439,#19440,#19441,#19442,#19443,#19444,#19445,
#19446,#19447,#19448,#19449,#19450,#19451,#19452,#19453,#19454,#19455,#19456,
#19457,#19458,#19459,#19460,#19461,#19462,#19463,#19464,#19465,#19466,#19467),
(#19468,#19469,#19470,#19471,#19472,#19473,#19474,#19475,#19476,#19477,
#19478,#19479,#19480,#19481,#19482,#19483,#19484,#19485,#19486,#19487,#19488,
#19489,#19490,#19491,#19492,#19493,#19494,#19495,#19496,#19497,#19498,#19499,
#19500,#19501,#19502,#19503,#19504,#19505,#19506,#19507,#19508,#19509,#19510,
#19511,#19512,#19513,#19514,#19515,#19516,#19517,#19518,#19519,#19520,#19521,
#19522,#19523,#19524,#19525,#19526,#19527,#19528,#19529,#19530,#19531,#19532,
#19533,#19534,#19535,#19536,#19537,#19538,#19539,#19540,#19541,#19542,#19543,
#19544,#19545,#19546,#19547,#19548,#19549,#19550,#19551,#19552,#19553,#19554,
#19555,#19556,#19557),(#19558,#19559,#19560,#19561,#19562,#19563,#19564,
#19565,#19566,#19567,#19568,#19569,#19570,#19571,#19572,#19573,#19574,#19575,
#19576,#19577,#19578,#19579,#19580,#19581,#19582,#19583,#19584,#19585,#19586,
#19587,#19588,#19589,#19590,#19591,#19592,#19593,#19594,#19595,#19596,#19597,
#19598,#19599,#19600,#19601,#19602,#19603,#19604,#19605,#19606,#19607,#19608,
#19609,#19610,#19611,#19612,#19613,#19614,#19615,#19616,#19617,#19618,#19619,
#19620,#19621,#19622,#19623,#19624,#19625,#19626,#19627,#19628,#19629,#19630,
#19631,#19632,#19633,#19634,#19635,#19636,#19637,#19638,#19639,#19640,#19641,
#19642,#19643,#19644,#19645,#19646,#19647)),.UNSPECIFIED.,.F.,.F.,.F.,(4,
4),(4,1,1,1,1,1,1,1,1,1,1,1,1,1,1,1,1,1,1,1,1,1,1,1,1,1,1,1,1,1,1,1,1,1,
1,1,1,1,1,1,1,1,1,1,1,1,1,1,1,1,1,1,1,1,1,1,1,1,1,1,1,1,1,1,1,1,1,1,1,1,
1,1,1,1,1,1,1,1,1,1,1,1,1,1,1,1,1,4),(0.,0.0460148164544132),(8.31058692273971,
9.30873374912645,10.3068805755132,11.3050274018999,12.3031742282867,13.3013210546734,
14.2994678810601,15.2976147074469,16.2957615338336,17.2939083602203,18.2920551866071,
19.2902020129938,20.2883488393806,21.2864956657673,22.284642492154,23.2827893185408,
24.2809361449275,25.2790829713142,26.277229797701,27.2753766240877,28.2735234504744,
29.2716702768612,30.2698171032479,31.2679639296347,32.2661107560214,33.2642575824081,
34.2624044087949,35.2605512351816,36.2586980615683,37.2568448879551,38.2549917143418,
39.2531385407286,40.2512853671153,41.249432193502,42.2475790198888,43.2457258462755,
44.2438726726622,45.242019499049,46.2401663254357,47.2383131518225,48.2364599782092,
49.2346068045959,50.2327536309827,51.2309004573694,52.2290472837561,53.2271941101429,
54.2253409365296,55.2234877629163,56.2216345893031,57.2197814156898,58.2179282420766,
59.2160750684633,60.21422189485,61.2123687212368,62.2105155476235,63.2086623740102,
64.206809200397,65.2049560267837,66.2031028531704,67.2012496795572,68.1993965059439,
69.1975433323307,70.1956901587174,71.1938369851041,72.1919838114909,73.1901306378776,
74.1882774642643,75.1864242906511,76.1845711170378,77.1827179434245,78.1808647698113,
79.179011596198,80.1771584225848,81.1753052489715,82.1734520753582,83.171598901745,
84.1697457281317,85.1678925545184,86.1660393809052,87.1641862072919,88.1623330336787,
89.1604798600654,90.1586266864521,91.1567735128389,92.1549203392256,93.1530671656123,
94.1512139919991,95.1493608183858),.UNSPECIFIED.);
#356=B_SPLINE_CURVE_WITH_KNOTS('',3,(#17593,#17594,#17595,#17596,#17597,
#17598,#17599,#17600,#17601,#17602),.UNSPECIFIED.,.F.,.F.,(4,3,3,4),(-4.09254174883832,
-3.98934747117026,-2.99201060337769,-2.06514013327813),.UNSPECIFIED.);
#357=B_SPLINE_CURVE_WITH_KNOTS('',3,(#17605,#17606,#17607,#17608,#17609,
#17610,#17611),.UNSPECIFIED.,.F.,.F.,(4,3,4),(0.,0.998146826386724,1.11419103802952),
 .UNSPECIFIED.);
#358=B_SPLINE_CURVE_WITH_KNOTS('',3,(#17616,#17617,#17618,#17619,#17620,
#17621,#17622,#17623,#17624,#17625,#17626,#17627,#17628,#17629,#17630,#17631,
#17632,#17633,#17634,#17635,#17636,#17637),.UNSPECIFIED.,.F.,.F.,(4,3,3,
3,3,3,3,4),(-10.3757270560179,-9.97336867792565,-8.97603181013308,-7.97869494234052,
-6.98135807454796,-5.98402120675539,-4.98668433896283,-4.09254174883832),
 .UNSPECIFIED.);
#359=B_SPLINE_CURVE_WITH_KNOTS('',3,(#17638,#17639,#17640,#17641,#17642,
#17643,#17644,#17645,#17646,#17647,#17648,#17649,#17650,#17651,#17652,#17653,
#17654,#17655,#17656,#17657,#17658,#17659),.UNSPECIFIED.,.F.,.F.,(4,3,3,
3,3,3,3,4),(1.11419103802952,1.99629365277347,2.9944404791602,3.99258730554694,
4.99073413193368,5.98888095832042,6.98702778470716,7.39737634520911),
 .UNSPECIFIED.);
#360=B_SPLINE_CURVE_WITH_KNOTS('',3,(#17664,#17665,#17666,#17667,#17668,
#17669,#17670,#17671,#17672,#17673,#17674,#17675,#17676,#17677,#17678,#17679,
#17680,#17681,#17682,#17683,#17684,#17685),.UNSPECIFIED.,.F.,.F.,(4,3,3,
3,3,3,3,4),(-16.6589123631975,-15.957389884681,-14.9600530168885,-13.9627161490959,
-12.9653792813033,-11.9680424135108,-10.9707055457182,-10.3757270560179),
 .UNSPECIFIED.);
#361=B_SPLINE_CURVE_WITH_KNOTS('',3,(#17686,#17687,#17688,#17689,#17690,
#17691,#17692,#17693,#17694,#17695,#17696,#17697,#17698,#17699,#17700,#17701,
#17702,#17703,#17704,#17705,#17706,#17707),.UNSPECIFIED.,.F.,.F.,(4,3,3,
3,3,3,3,4),(7.39737634520911,7.9851746110939,8.98332143748063,9.98146826386737,
10.9796150902541,11.9777619166408,12.9759087430276,13.6805616523887),
 .UNSPECIFIED.);
#362=B_SPLINE_CURVE_WITH_KNOTS('',3,(#17712,#17713,#17714,#17715,#17716,
#17717,#17718,#17719,#17720,#17721,#17722,#17723,#17724,#17725,#17726,#17727,
#17728,#17729,#17730,#17731,#17732,#17733,#17734,#17735,#17736),
 .UNSPECIFIED.,.F.,.F.,(4,3,3,3,3,3,3,3,4),(-22.9420976703771,-22.938747959229,
-21.9414110914364,-20.9440742236439,-19.9467373558513,-18.9494004880587,
-17.9520636202662,-16.9547267524736,-16.6589123631975),.UNSPECIFIED.);
#363=B_SPLINE_CURVE_WITH_KNOTS('',3,(#17737,#17738,#17739,#17740,#17741,
#17742,#17743,#17744,#17745,#17746,#17747,#17748,#17749,#17750,#17751,#17752,
#17753,#17754,#17755,#17756,#17757,#17758),.UNSPECIFIED.,.F.,.F.,(4,3,3,
3,3,3,3,4),(13.6805616523887,13.9740555694143,14.972202395801,15.9703492221878,
16.9684960485745,17.9666428749613,18.964789701348,19.9637469595683),
 .UNSPECIFIED.);
#364=B_SPLINE_CURVE_WITH_KNOTS('',3,(#17763,#17764,#17765,#17766,#17767,
#17768,#17769,#17770,#17771,#17772,#17773,#17774,#17775,#17776,#17777,#17778,
#17779,#17780,#17781,#17782,#17783,#17784),.UNSPECIFIED.,.F.,.F.,(4,3,3,
3,3,3,3,4),(-29.2252829775567,-28.9227691659844,-27.9254322981918,-26.9280954303993,
-25.9307585626067,-24.9334216948141,-23.9360848270216,-22.9420976703771),
 .UNSPECIFIED.);
#365=B_SPLINE_CURVE_WITH_KNOTS('',3,(#17785,#17786,#17787,#17788,#17789,
#17790,#17791,#17792,#17793,#17794,#17795,#17796,#17797,#17798,#17799,#17800,
#17801,#17802,#17803,#17804,#17805,#17806),.UNSPECIFIED.,.F.,.F.,(4,3,3,
3,3,3,3,4),(19.9637469595683,20.9610833541215,21.9592301805082,22.9573770068949,
23.9555238332817,24.9536706596684,25.9518174860552,26.2469322667479),
 .UNSPECIFIED.);
#366=B_SPLINE_CURVE_WITH_KNOTS('',3,(#17811,#17812,#17813,#17814,#17815,
#17816,#17817,#17818,#17819,#17820,#17821,#17822,#17823,#17824,#17825,#17826,
#17827,#17828,#17829,#17830,#17831,#17832),.UNSPECIFIED.,.F.,.F.,(4,3,3,
3,3,3,3,4),(-35.5084682847363,-34.9067903727398,-33.9094535049472,-32.9121166371546,
-31.9147797693621,-30.9174429015695,-29.9201060337769,-29.2252829775567),
 .UNSPECIFIED.);
#367=B_SPLINE_CURVE_WITH_KNOTS('',3,(#17833,#17834,#17835,#17836,#17837,
#17838,#17839,#17840,#17841,#17842,#17843,#17844,#17845,#17846,#17847,#17848,
#17849,#17850,#17851,#17852,#17853,#17854),.UNSPECIFIED.,.F.,.F.,(4,3,3,
3,3,3,3,4),(26.2469322667479,26.9499643124419,27.9481111388286,28.9462579652154,
29.9444047916021,30.9425516179888,31.9406984443756,32.5301175739274),
 .UNSPECIFIED.);
#368=B_SPLINE_CURVE_WITH_KNOTS('',3,(#17859,#17860,#17861,#17862,#17863,
#17864,#17865,#17866,#17867,#17868,#17869,#17870,#17871,#17872,#17873,#17874,
#17875,#17876,#17877,#17878,#17879,#17880),.UNSPECIFIED.,.F.,.F.,(4,3,3,
3,3,3,3,4),(-41.7916535919158,-40.8908115794952,-39.8934747117026,-38.89613784391,
-37.8988009761175,-36.9014641083249,-35.9041272405323,-35.5084682847363),
 .UNSPECIFIED.);
#369=B_SPLINE_CURVE_WITH_KNOTS('',3,(#17881,#17882,#17883,#17884,#17885,
#17886,#17887,#17888,#17889,#17890,#17891,#17892,#17893,#17894,#17895,#17896,
#17897,#17898,#17899,#17900,#17901,#17902),.UNSPECIFIED.,.F.,.F.,(4,3,3,
3,3,3,3,4),(32.5301175739274,32.9388452707623,33.9369920971491,34.9351389235358,
35.9332857499225,36.9314325763093,37.929579402696,38.813302881107),
 .UNSPECIFIED.);
#370=B_SPLINE_CURVE_WITH_KNOTS('',3,(#17907,#17908,#17909,#17910,#17911,
#17912,#17913,#17914,#17915,#17916,#17917,#17918,#17919,#17920,#17921,#17922,
#17923,#17924,#17925,#17926,#17927,#17928,#17929,#17930,#17931),
 .UNSPECIFIED.,.F.,.F.,(4,3,3,3,3,3,3,3,4),(-48.0748388990954,-47.8721696540431,
-46.8748327862506,-45.877495918458,-44.8801590506654,-43.8828221828729,
-42.8854853150803,-41.8881484472877,-41.7916535919158),.UNSPECIFIED.);
#371=B_SPLINE_CURVE_WITH_KNOTS('',3,(#17932,#17933,#17934,#17935,#17936,
#17937,#17938,#17939,#17940,#17941,#17942,#17943,#17944,#17945,#17946,#17947,
#17948,#17949,#17950,#17951,#17952,#17953,#17954,#17955,#17956),
 .UNSPECIFIED.,.F.,.F.,(4,3,3,3,3,3,3,3,4),(38.813302881107,38.9277262290827,
39.9258730554695,40.9240198818562,41.9221667082429,42.9203135346297,43.9184603610164,
44.9166071874032,45.0964881882866),.UNSPECIFIED.);
#372=B_SPLINE_CURVE_WITH_KNOTS('',3,(#17961,#17962,#17963,#17964,#17965,
#17966,#17967,#17968,#17969,#17970,#17971,#17972,#17973,#17974,#17975,#17976,
#17977,#17978,#17979,#17980,#17981,#17982),.UNSPECIFIED.,.F.,.F.,(4,3,3,
3,3,3,3,4),(-54.358024206275,-53.8561908607985,-52.8588539930059,-51.8615171252134,
-50.8641802574208,-49.8668433896283,-48.8695065218357,-48.0748388990954),
 .UNSPECIFIED.);
#373=B_SPLINE_CURVE_WITH_KNOTS('',3,(#17983,#17984,#17985,#17986,#17987,
#17988,#17989,#17990,#17991,#17992,#17993,#17994,#17995,#17996,#17997,#17998,
#17999,#18000,#18001,#18002,#18003,#18004),.UNSPECIFIED.,.F.,.F.,(4,3,3,
3,3,3,3,4),(45.0964881882866,45.9147540137899,46.9129008401766,47.9110476665634,
48.9091944929501,49.9073413193368,50.9054881457236,51.3796734954662),
 .UNSPECIFIED.);
#374=B_SPLINE_CURVE_WITH_KNOTS('',3,(#18009,#18010,#18011,#18012,#18013,
#18014,#18015,#18016,#18017,#18018,#18019,#18020,#18021,#18022,#18023,#18024,
#18025,#18026,#18027,#18028,#18029,#18030),.UNSPECIFIED.,.F.,.F.,(4,3,3,
3,3,3,3,4),(-60.6412095134546,-59.8402120675539,-58.8428751997613,-57.8455383319688,
-56.8482014641762,-55.8508645963836,-54.8535277285911,-54.358024206275),
 .UNSPECIFIED.);
#375=B_SPLINE_CURVE_WITH_KNOTS('',3,(#18031,#18032,#18033,#18034,#18035,
#18036,#18037,#18038,#18039,#18040,#18041,#18042,#18043,#18044,#18045,#18046,
#18047,#18048,#18049,#18050,#18051,#18052),.UNSPECIFIED.,.F.,.F.,(4,3,3,
3,3,3,3,4),(51.3796734954662,51.9036349721103,52.901781798497,53.8999286248838,
54.8980754512705,55.8962222776573,56.894369104044,57.6628588026458),
 .UNSPECIFIED.);
#376=B_SPLINE_CURVE_WITH_KNOTS('',3,(#18057,#18058,#18059,#18060,#18061,
#18062,#18063,#18064,#18065,#18066,#18067,#18068,#18069,#18070,#18071,#18072,
#18073,#18074,#18075,#18076,#18077,#18078,#18079,#18080,#18081),
 .UNSPECIFIED.,.F.,.F.,(4,3,3,3,3,3,3,3,4),(-66.9243948206342,-66.8215701421018,
-65.8242332743093,-64.8268964065167,-63.8295595387242,-62.8322226709316,
-61.834885803139,-60.8375489353465,-60.6412095134546),.UNSPECIFIED.);
#377=B_SPLINE_CURVE_WITH_KNOTS('',3,(#18082,#18083,#18084,#18085,#18086,
#18087,#18088,#18089,#18090,#18091,#18092,#18093,#18094,#18095,#18096,#18097,
#18098,#18099,#18100,#18101,#18102,#18103,#18104,#18105,#18106),
 .UNSPECIFIED.,.F.,.F.,(4,3,3,3,3,3,3,3,4),(57.6628588026458,57.8925159304307,
58.8906627568175,59.8888095832042,60.8869564095909,61.8851032359777,62.8832500623644,
63.8813968887512,63.9460441098254),.UNSPECIFIED.);
#378=B_SPLINE_CURVE_WITH_KNOTS('',3,(#18111,#18112,#18113,#18114,#18115,
#18116,#18117,#18118,#18119,#18120,#18121,#18122,#18123,#18124,#18125,#18126,
#18127,#18128,#18129,#18130,#18131,#18132),.UNSPECIFIED.,.F.,.F.,(4,3,3,
3,3,3,3,4),(-73.2075801278138,-72.8055913488572,-71.8082544810647,-70.8109176132721,
-69.8135807454795,-68.816243877687,-67.8189070098944,-66.9243948206342),
 .UNSPECIFIED.);
#379=B_SPLINE_CURVE_WITH_KNOTS('',3,(#18133,#18134,#18135,#18136,#18137,
#18138,#18139,#18140,#18141,#18142,#18143,#18144,#18145,#18146,#18147,#18148,
#18149,#18150,#18151,#18152,#18153,#18154),.UNSPECIFIED.,.F.,.F.,(4,3,3,
3,3,3,3,4),(63.9460441098254,64.8795437151379,65.8776905415246,66.8758373679114,
67.8739841942981,68.8721310206848,69.8702778470716,70.229229417005),
 .UNSPECIFIED.);
#380=B_SPLINE_CURVE_WITH_KNOTS('',3,(#18159,#18160,#18161,#18162,#18163,
#18164,#18165,#18166,#18167,#18168,#18169,#18170,#18171,#18172,#18173,#18174,
#18175,#18176,#18177,#18178,#18179,#18180),.UNSPECIFIED.,.F.,.F.,(4,3,3,
3,3,3,3,4),(-79.4907654349934,-78.7896125556126,-77.7922756878201,-76.7949388200275,
-75.7976019522349,-74.8002650844424,-73.8029282166498,-73.2075801278138),
 .UNSPECIFIED.);
#381=B_SPLINE_CURVE_WITH_KNOTS('',3,(#18181,#18182,#18183,#18184,#18185,
#18186,#18187,#18188,#18189,#18190,#18191,#18192,#18193,#18194,#18195,#18196,
#18197,#18198,#18199,#18200,#18201,#18202),.UNSPECIFIED.,.F.,.F.,(4,3,3,
3,3,3,3,4),(70.229229417005,70.8684246734583,71.8665714998451,72.8647183262318,
73.8628651526185,74.8610119790053,75.859158805392,76.5124147241846),
 .UNSPECIFIED.);
#382=B_SPLINE_CURVE_WITH_KNOTS('',3,(#18208,#18209,#18210,#18211,#18212,
#18213,#18214,#18215,#18216),.UNSPECIFIED.,.F.,.F.,(4,1,1,1,1,1,4),(91.106186954104,
91.4023709425158,92.3997078103083,93.3970446781009,94.3943815458935,95.391718413686,
96.3890552814786),.UNSPECIFIED.);
#383=B_SPLINE_CURVE_WITH_KNOTS('',3,(#18219,#18220,#18221,#18222,#18223,
#18224,#18225,#18226),.UNSPECIFIED.,.F.,.F.,(4,1,1,1,1,4),(91.106186954104,
91.1567735128389,92.1549203392256,93.1530671656123,94.1512139919991,95.1493608183858),
 .UNSPECIFIED.);
#384=B_SPLINE_CURVE_WITH_KNOTS('',3,(#18231,#18232,#18233,#18234,#18235,
#18236,#18237,#18238,#18239,#18240),.UNSPECIFIED.,.F.,.F.,(4,1,1,1,1,1,
1,4),(84.8230016469244,85.4183497357604,86.4156866035529,87.4130234713455,
88.4103603391381,89.4076972069306,90.4050340747232,91.106186954104),
 .UNSPECIFIED.);
#385=B_SPLINE_CURVE_WITH_KNOTS('',3,(#18241,#18242,#18243,#18244,#18245,
#18246,#18247,#18248,#18249,#18250),.UNSPECIFIED.,.F.,.F.,(4,1,1,1,1,1,
1,4),(84.8230016469244,85.1678925545184,86.1660393809052,87.1641862072919,
88.1623330336787,89.1604798600654,90.1586266864521,91.106186954104),
 .UNSPECIFIED.);
#386=B_SPLINE_CURVE_WITH_KNOTS('',3,(#18255,#18256,#18257,#18258,#18259,
#18260,#18261,#18262,#18263,#18264),.UNSPECIFIED.,.F.,.F.,(4,1,1,1,1,1,
1,4),(78.5398163397448,79.434328529005,80.4316653967976,81.4290022645901,
82.4263391323827,83.4236760001752,84.4210128679678,84.8230016469244),
 .UNSPECIFIED.);
#387=B_SPLINE_CURVE_WITH_KNOTS('',3,(#18265,#18266,#18267,#18268,#18269,
#18270,#18271,#18272,#18273,#18274),.UNSPECIFIED.,.F.,.F.,(4,1,1,1,1,1,
1,4),(78.5398163397448,79.179011596198,80.1771584225848,81.1753052489715,
82.1734520753582,83.171598901745,84.1697457281317,84.8230016469244),
 .UNSPECIFIED.);
#388=B_SPLINE_CURVE_WITH_KNOTS('',3,(#18279,#18280,#18281,#18282,#18283,
#18284,#18285,#18286,#18287,#18288,#18289),.UNSPECIFIED.,.F.,.F.,(4,1,1,
1,1,1,1,1,4),(72.2566310325652,72.452970454457,73.4503073222496,74.4476441900422,
75.4449810578347,76.4423179256273,77.4396547934198,78.4369916612124,78.5398163397448),
 .UNSPECIFIED.);
#389=B_SPLINE_CURVE_WITH_KNOTS('',3,(#18290,#18291,#18292,#18293,#18294,
#18295,#18296,#18297,#18298,#18299),.UNSPECIFIED.,.F.,.F.,(4,1,1,1,1,1,
1,4),(72.2566310325652,73.1901306378776,74.1882774642643,75.1864242906511,
76.1845711170378,77.1827179434245,78.1808647698113,78.5398163397448),
 .UNSPECIFIED.);
#390=B_SPLINE_CURVE_WITH_KNOTS('',3,(#18304,#18305,#18306,#18307,#18308,
#18309,#18310,#18311,#18312,#18313),.UNSPECIFIED.,.F.,.F.,(4,1,1,1,1,1,
1,4),(65.9734457253856,66.4689492477016,67.4662861154942,68.4636229832868,
69.4609598510793,70.4582967188719,71.4556335866645,72.2566310325652),
 .UNSPECIFIED.);
#391=B_SPLINE_CURVE_WITH_KNOTS('',3,(#18314,#18315,#18316,#18317,#18318,
#18319,#18320,#18321,#18322,#18323,#18324),.UNSPECIFIED.,.F.,.F.,(4,1,1,
1,1,1,1,1,4),(65.9734457253856,66.2031028531704,67.2012496795572,68.1993965059439,
69.1975433323307,70.1956901587174,71.1938369851041,72.1919838114909,72.2566310325652),
 .UNSPECIFIED.);
#392=B_SPLINE_CURVE_WITH_KNOTS('',3,(#18329,#18330,#18331,#18332,#18333,
#18334,#18335,#18336,#18337,#18338),.UNSPECIFIED.,.F.,.F.,(4,1,1,1,1,1,
1,4),(59.690260418206,60.4849280409463,61.4822649087388,62.4796017765314,
63.4769386443239,64.4742755121165,65.4716123799091,65.9734457253856),
 .UNSPECIFIED.);
#393=B_SPLINE_CURVE_WITH_KNOTS('',3,(#18339,#18340,#18341,#18342,#18343,
#18344,#18345,#18346,#18347,#18348),.UNSPECIFIED.,.F.,.F.,(4,1,1,1,1,1,
1,4),(59.690260418206,60.21422189485,61.2123687212368,62.2105155476235,
63.2086623740102,64.206809200397,65.2049560267837,65.9734457253856),
 .UNSPECIFIED.);
#394=B_SPLINE_CURVE_WITH_KNOTS('',3,(#18353,#18354,#18355,#18356,#18357,
#18358,#18359,#18360,#18361,#18362,#18363),.UNSPECIFIED.,.F.,.F.,(4,1,1,
1,1,1,1,1,4),(53.4070751110265,53.5035699663983,54.5009068341909,55.4982437019834,
56.495580569776,57.4929174375686,58.4902543053611,59.4875911731537,59.690260418206),
 .UNSPECIFIED.);
#395=B_SPLINE_CURVE_WITH_KNOTS('',3,(#18364,#18365,#18366,#18367,#18368,
#18369,#18370,#18371,#18372,#18373),.UNSPECIFIED.,.F.,.F.,(4,1,1,1,1,1,
1,4),(53.4070751110264,54.2253409365296,55.2234877629163,56.2216345893031,
57.2197814156898,58.2179282420766,59.2160750684633,59.690260418206),
 .UNSPECIFIED.);
#396=B_SPLINE_CURVE_WITH_KNOTS('',3,(#18378,#18379,#18380,#18381,#18382,
#18383,#18384,#18385,#18386,#18387),.UNSPECIFIED.,.F.,.F.,(4,1,1,1,1,1,
1,4),(47.1238898038469,47.5195487596429,48.5168856274355,49.514222495228,
50.5115593630206,51.5088962308132,52.5062330986057,53.4070751110265),
 .UNSPECIFIED.);
#397=B_SPLINE_CURVE_WITH_KNOTS('',3,(#18388,#18389,#18390,#18391,#18392,
#18393,#18394,#18395,#18396,#18397,#18398),.UNSPECIFIED.,.F.,.F.,(4,1,1,
1,1,1,1,1,4),(47.1238898038468,47.2383131518225,48.2364599782092,49.2346068045959,
50.2327536309827,51.2309004573694,52.2290472837561,53.2271941101429,53.4070751110264),
 .UNSPECIFIED.);
#398=B_SPLINE_CURVE_WITH_KNOTS('',3,(#18403,#18404,#18405,#18406,#18407,
#18408,#18409,#18410,#18411,#18412),.UNSPECIFIED.,.F.,.F.,(4,1,1,1,1,1,
1,4),(40.8407044966673,41.5355275528875,42.5328644206801,43.5302012884726,
44.5275381562652,45.5248750240578,46.5222118918503,47.1238898038469),
 .UNSPECIFIED.);
#399=B_SPLINE_CURVE_WITH_KNOTS('',3,(#18413,#18414,#18415,#18416,#18417,
#18418,#18419,#18420,#18421,#18422),.UNSPECIFIED.,.F.,.F.,(4,1,1,1,1,1,
1,4),(40.8407044966673,41.249432193502,42.2475790198888,43.2457258462755,
44.2438726726622,45.242019499049,46.2401663254357,47.1238898038468),
 .UNSPECIFIED.);
#400=B_SPLINE_CURVE_WITH_KNOTS('',3,(#18427,#18428,#18429,#18430,#18431,
#18432,#18433,#18434,#18435,#18436),.UNSPECIFIED.,.F.,.F.,(4,1,1,1,1,1,
1,4),(34.5575191894877,35.5515063461321,36.5488432139247,37.5461800817173,
38.5435169495098,39.5408538173024,40.538190685095,40.8407044966673),
 .UNSPECIFIED.);
#401=B_SPLINE_CURVE_WITH_KNOTS('',3,(#18437,#18438,#18439,#18440,#18441,
#18442,#18443,#18444,#18445,#18446),.UNSPECIFIED.,.F.,.F.,(4,1,1,1,1,1,
1,4),(34.5575191894876,35.2605512351816,36.2586980615683,37.2568448879551,
38.2549917143418,39.2531385407286,40.2512853671153,40.8407044966673),
 .UNSPECIFIED.);
#402=B_SPLINE_CURVE_WITH_KNOTS('',3,(#18451,#18452,#18453,#18454,#18455,
#18456,#18457,#18458,#18459,#18460,#18461),.UNSPECIFIED.,.F.,.F.,(4,1,1,
1,1,1,1,1,4),(28.2743338823081,28.5701482715842,29.5674851393767,30.5648220071693,
31.5621588749619,32.5594957427544,33.556832610547,34.5541694783396,34.5575191894877),
 .UNSPECIFIED.);
#403=B_SPLINE_CURVE_WITH_KNOTS('',3,(#18462,#18463,#18464,#18465,#18466,
#18467,#18468,#18469,#18470,#18471),.UNSPECIFIED.,.F.,.F.,(4,1,1,1,1,1,
1,4),(28.2743338823081,29.2716702768612,30.2698171032479,31.2679639296347,
32.2661107560214,33.2642575824081,34.2624044087949,34.5575191894876),
 .UNSPECIFIED.);
#404=B_SPLINE_CURVE_WITH_KNOTS('',3,(#18476,#18477,#18478,#18479,#18480,
#18481,#18482,#18483,#18484,#18485),.UNSPECIFIED.,.F.,.F.,(4,1,1,1,1,1,
1,4),(21.9911485751285,22.5861270648288,23.5834639326213,24.5808008004139,
25.5781376682065,26.575474535999,27.5728114037916,28.2743338823081),
 .UNSPECIFIED.);
#405=B_SPLINE_CURVE_WITH_KNOTS('',3,(#18486,#18487,#18488,#18489,#18490,
#18491,#18492,#18493,#18494,#18495,#18496),.UNSPECIFIED.,.F.,.F.,(4,1,1,
1,1,1,1,1,4),(21.9911485751285,22.284642492154,23.2827893185408,24.2809361449275,
25.2790829713142,26.277229797701,27.2753766240877,28.2735234504744,28.2743338823081),
 .UNSPECIFIED.);
#406=B_SPLINE_CURVE_WITH_KNOTS('',3,(#18501,#18502,#18503,#18504,#18505,
#18506,#18507,#18508,#18509,#18510),.UNSPECIFIED.,.F.,.F.,(4,1,1,1,1,1,
1,4),(15.7079632679489,16.6021058580734,17.599442725866,18.5967795936585,
19.5941164614511,20.5914533292437,21.5887901970362,21.9911485751285),
 .UNSPECIFIED.);
#407=B_SPLINE_CURVE_WITH_KNOTS('',3,(#18511,#18512,#18513,#18514,#18515,
#18516,#18517,#18518,#18519,#18520),.UNSPECIFIED.,.F.,.F.,(4,1,1,1,1,1,
1,4),(15.7079632679489,16.2957615338336,17.2939083602203,18.2920551866071,
19.2902020129938,20.2883488393806,21.2864956657673,21.9911485751285),
 .UNSPECIFIED.);
#408=B_SPLINE_CURVE_WITH_KNOTS('',3,(#18523,#18524,#18525,#18526,#18527,
#18528,#18529,#18530,#18531,#18532,#18533,#18534,#18535,#18536,#18537,#18538,
#18539,#18540,#18541,#18542,#18543,#18544,#18545,#18546,#18547,#18548,#18549,
#18550,#18551,#18552,#18553,#18554,#18555,#18556,#18557,#18558,#18559,#18560,
#18561,#18562,#18563,#18564,#18565,#18566,#18567,#18568,#18569,#18570,#18571,
#18572,#18573,#18574,#18575,#18576,#18577,#18578,#18579,#18580,#18581,#18582,
#18583,#18584,#18585,#18586,#18587,#18588,#18589,#18590,#18591,#18592,#18593,
#18594,#18595,#18596,#18597,#18598,#18599,#18600,#18601,#18602,#18603,#18604,
#18605,#18606,#18607,#18608,#18609,#18610,#18611,#18612,#18613,#18614,#18615,
#18616,#18617,#18618,#18619,#18620,#18621,#18622,#18623,#18624,#18625,#18626,
#18627,#18628,#18629,#18630,#18631,#18632,#18633,#18634,#18635,#18636,#18637,
#18638,#18639,#18640,#18641,#18642,#18643,#18644,#18645,#18646,#18647,#18648,
#18649,#18650,#18651,#18652,#18653,#18654,#18655,#18656,#18657,#18658,#18659,
#18660,#18661,#18662,#18663,#18664,#18665,#18666,#18667,#18668,#18669,#18670,
#18671,#18672,#18673,#18674,#18675,#18676,#18677,#18678,#18679,#18680,#18681,
#18682,#18683,#18684,#18685),.UNSPECIFIED.,.F.,.F.,(4,3,3,3,3,3,3,3,3,3,
3,3,3,3,3,3,3,3,3,3,3,3,3,3,3,3,3,3,3,3,3,3,3,3,3,3,3,3,3,3,3,3,3,3,3,3,
3,3,3,3,3,3,3,3,4),(-0.996917990983859,-0.978871687936248,-0.96110860637064,
-0.951564552512273,-0.947875257318018,-0.928946481496676,-0.909864161986251,
-0.904894692675967,-0.901793526230914,-0.882487196974259,-0.863299579085687,
-0.850033307248536,-0.842040929909056,-0.838709317247451,-0.836767035411385,
-0.818231407546695,-0.79887889956488,-0.782708868337739,-0.778189567206005,
-0.77429492151425,-0.754727508647775,-0.734919748031306,-0.718569473460416,
-0.712593983904593,-0.709109999006969,-0.689189825792525,-0.669518649747745,
-0.649842645634906,-0.64559751135709,-0.64260293594092,-0.622842747933918,
-0.602674899262203,-0.589266851632816,-0.58051316491066,-0.577021522026438,
-0.556531415549597,-0.536105697847013,-0.515758108037061,-0.510662639580459,
-0.506544813616949,-0.495410518227108,-0.475531470589818,-0.455379232363541,
-0.446467573071616,-0.440751338400796,-0.437135243079585,-0.416452388484242,
-0.395479231887803,-0.375187815110753,-0.368827535471261,-0.36537325419559,
-0.344179044892366,-0.32336231319227,-0.314313564779604,-0.304957861769162),
 .UNSPECIFIED.);
#409=B_SPLINE_CURVE_WITH_KNOTS('',3,(#18687,#18688,#18689,#18690,#18691,
#18692,#18693,#18694,#18695,#18696,#18697,#18698,#18699,#18700,#18701,#18702,
#18703,#18704,#18705,#18706,#18707,#18708,#18709,#18710,#18711,#18712,#18713,
#18714,#18715,#18716,#18717,#18718,#18719,#18720,#18721,#18722,#18723,#18724,
#18725,#18726,#18727,#18728,#18729,#18730,#18731,#18732,#18733,#18734,#18735,
#18736,#18737,#18738,#18739,#18740,#18741,#18742,#18743,#18744),
 .UNSPECIFIED.,.F.,.F.,(4,3,3,3,3,3,3,3,3,3,3,3,3,3,3,3,3,3,3,4),(-0.271362855059931,
-0.249815153611103,-0.228817936840513,-0.21475709335129,-0.20269615019584,
-0.199258579296682,-0.179079219908023,-0.172574562883619,-0.151002742523167,
-0.132127399707771,-0.128545224966699,-0.108660381316369,-0.088904641890274,
-0.0695673848931777,-0.0643977176859483,-0.0611873514593056,-0.0424333152675423,
-0.0240015440670001,-0.00610711498195276,0.),.UNSPECIFIED.);
#410=B_SPLINE_CURVE_WITH_KNOTS('',3,(#18747,#18748,#18749,#18750,#18751,
#18752,#18753,#18754,#18755,#18756,#18757,#18758,#18759,#18760,#18761,#18762,
#18763,#18764,#18765,#18766,#18767,#18768,#18769,#18770,#18771,#18772,#18773,
#18774,#18775,#18776,#18777,#18778,#18779,#18780,#18781,#18782,#18783,#18784,
#18785,#18786,#18787,#18788,#18789,#18790,#18791,#18792,#18793,#18794,#18795,
#18796,#18797,#18798,#18799,#18800,#18801,#18802,#18803,#18804,#18805,#18806,
#18807,#18808,#18809,#18810),.UNSPECIFIED.,.F.,.F.,(4,3,3,3,3,3,3,3,3,3,
3,3,3,3,3,3,3,3,3,3,3,4),(-0.304957861769162,-0.297138437894475,-0.27579526247451,
-0.25452115728438,-0.238505141940676,-0.229387728747905,-0.225368790891129,
-0.221917825979367,-0.200380627888395,-0.178797401191701,-0.157590348312134,
-0.15077543359462,-0.1472283770012,-0.12639303453475,-0.105100297430208,
-0.083375892217648,-0.0782531846850942,-0.0733795998480499,-0.0515968866484263,
-0.0295071888683422,-0.00749310652115608,0.),.UNSPECIFIED.);
#411=B_SPLINE_CURVE_WITH_KNOTS('',3,(#19167,#19168,#19169,#19170,#19171,
#19172,#19173,#19174),.UNSPECIFIED.,.F.,.F.,(4,1,1,1,1,4),(11.6154215191106,
12.6127583869031,13.6100952546957,14.6074321224883,15.6047689902808,15.7079632679489),
 .UNSPECIFIED.);
#412=B_SPLINE_CURVE_WITH_KNOTS('',3,(#19175,#19176,#19177,#19178,#19179,
#19180,#19181,#19182,#19183,#19184,#19185,#19186,#19187,#19188,#19189,#19190,
#19191,#19192,#19193,#19194,#19195,#19196,#19197,#19198,#19199,#19200,#19201,
#19202,#19203,#19204,#19205,#19206,#19207,#19208,#19209,#19210,#19211,#19212,
#19213,#19214,#19215,#19216,#19217,#19218,#19219,#19220,#19221,#19222,#19223,
#19224,#19225,#19226,#19227,#19228,#19229,#19230,#19231,#19232,#19233,#19234,
#19235,#19236,#19237,#19238,#19239,#19240,#19241,#19242,#19243,#19244,#19245,
#19246,#19247,#19248,#19249,#19250,#19251,#19252,#19253,#19254,#19255,#19256,
#19257,#19258,#19259),.UNSPECIFIED.,.F.,.F.,(4,3,3,3,3,3,3,3,3,3,3,3,3,
3,3,3,3,3,3,3,3,3,3,3,3,3,3,3,4),(-0.364629307890664,-0.350886157932352,
-0.329296891193796,-0.318978960138819,-0.313744359949613,-0.309365983727222,
-0.288043719998357,-0.272809977372963,-0.264007580396482,-0.260298494201204,
-0.239567406370511,-0.219347171290133,-0.206053823216401,-0.194877404256716,
-0.191399198693004,-0.171813503246808,-0.166173778995206,-0.145402056620805,
-0.126707179806039,-0.123380359543154,-0.103925995354622,-0.0845486906012833,
-0.0655680939453014,-0.062174737667072,-0.0589393440631834,-0.040349155528949,
-0.0220933089917935,-0.00442011167346308,0.),.UNSPECIFIED.);
#413=B_SPLINE_CURVE_WITH_KNOTS('',3,(#19260,#19261,#19262,#19263,#19264,
#19265,#19266,#19267,#19268,#19269,#19270,#19271,#19272,#19273,#19274,#19275),
 .UNSPECIFIED.,.F.,.F.,(4,3,3,3,3,4),(-83.2618462600588,-82.7789600267829,
-81.7816231589903,-80.7842862911978,-79.7869494234052,-79.4907654349934),
 .UNSPECIFIED.);
#414=B_SPLINE_CURVE_WITH_KNOTS('',3,(#19278,#19279,#19280,#19281,#19282,
#19283,#19284,#19285,#19286),.UNSPECIFIED.,.F.,.F.,(4,1,1,1,1,1,4),(10.3757270560178,
11.3050274018999,12.3031742282867,13.3013210546734,14.2994678810601,15.2976147074469,
15.7079632679489),.UNSPECIFIED.);
#415=B_SPLINE_CURVE_WITH_KNOTS('',3,(#19648,#19649,#19650,#19651,#19652,
#19653,#19654,#19655,#19656,#19657,#19658,#19659,#19660,#19661,#19662,#19663,
#19664,#19665,#19666),.UNSPECIFIED.,.F.,.F.,(4,3,3,3,3,3,4),(76.5124147241846,
76.8573056317787,77.8554524581655,78.8535992845522,79.8517461109389,80.8498929373257,
81.1967061267808),.UNSPECIFIED.);
#416=B_SPLINE_CURVE_WITH_KNOTS('',3,(#19667,#19668,#19669,#19670,#19671,
#19672,#19673,#19674,#19675,#19676,#19677,#19678,#19679,#19680,#19681,#19682,
#19683,#19684,#19685,#19686,#19687,#19688,#19689,#19690,#19691,#19692,#19693,
#19694,#19695,#19696,#19697,#19698,#19699,#19700,#19701,#19702,#19703,#19704,
#19705,#19706,#19707,#19708,#19709,#19710,#19711,#19712,#19713,#19714,#19715,
#19716,#19717,#19718,#19719,#19720,#19721,#19722,#19723,#19724,#19725,#19726,
#19727,#19728,#19729,#19730,#19731,#19732,#19733,#19734,#19735,#19736,#19737,
#19738,#19739,#19740,#19741,#19742,#19743,#19744,#19745,#19746,#19747,#19748),
 .UNSPECIFIED.,.F.,.F.,(4,3,3,3,3,3,3,3,3,3,3,3,3,3,3,3,3,3,3,3,3,3,3,3,
3,3,3,4),(-0.366397579005846,-0.355505695503922,-0.337536360352733,-0.327287439123245,
-0.321639660907082,-0.302830467228198,-0.288380955593988,-0.281239733716652,
-0.277590426350317,-0.258149250115452,-0.238331803396096,-0.225557446085701,
-0.218431814193006,-0.214861428615519,-0.194431505887542,-0.187234374154516,
-0.167529878294284,-0.147391270254625,-0.143955108128756,-0.123477740220191,
-0.102569087702513,-0.0815018425023604,-0.0762248591763458,-0.0720591440818486,
-0.0504140066563087,-0.0287210039487855,-0.00749333703700768,0.),
 .UNSPECIFIED.);
#435=SHAPE_REPRESENTATION_RELATIONSHIP('SRR','None',#19953,#454);
#454=ADVANCED_BREP_SHAPE_REPRESENTATION('',(#492),#19862);
#473=STYLED_ITEM('',(#20044),#492);
#492=MANIFOLD_SOLID_BREP('Body1',#6442);
#912=LINE('',#17591,#1377);
#913=LINE('',#17615,#1378);
#914=LINE('',#17663,#1379);
#915=LINE('',#17711,#1380);
#916=LINE('',#17762,#1381);
#917=LINE('',#17810,#1382);
#918=LINE('',#17858,#1383);
#919=LINE('',#17906,#1384);
#920=LINE('',#17960,#1385);
#921=LINE('',#18008,#1386);
#922=LINE('',#18056,#1387);
#923=LINE('',#18110,#1388);
#924=LINE('',#18158,#1389);
#925=LINE('',#18206,#1390);
#926=LINE('',#18230,#1391);
#927=LINE('',#18254,#1392);
#928=LINE('',#18278,#1393);
#929=LINE('',#18303,#1394);
#930=LINE('',#18328,#1395);
#931=LINE('',#18352,#1396);
#932=LINE('',#18377,#1397);
#933=LINE('',#18402,#1398);
#934=LINE('',#18426,#1399);
#935=LINE('',#18450,#1400);
#936=LINE('',#18475,#1401);
#937=LINE('',#18500,#1402);
#938=LINE('',#18812,#1403);
#939=LINE('',#19753,#1404);
#940=LINE('',#19755,#1405);
#941=LINE('',#19757,#1406);
#942=LINE('',#19758,#1407);
#943=LINE('',#19761,#1408);
#944=LINE('',#19763,#1409);
#945=LINE('',#19764,#1410);
#946=LINE('',#19767,#1411);
#947=LINE('',#19769,#1412);
#948=LINE('',#19770,#1413);
#949=LINE('',#19773,#1414);
#950=LINE('',#19775,#1415);
#951=LINE('',#19776,#1416);
#952=LINE('',#19779,#1417);
#953=LINE('',#19781,#1418);
#954=LINE('',#19782,#1419);
#955=LINE('',#19784,#1420);
#956=LINE('',#19785,#1421);
#957=LINE('',#19792,#1422);
#1377=VECTOR('',#8542,2.);
#1378=VECTOR('',#8547,2.);
#1379=VECTOR('',#8550,2.);
#1380=VECTOR('',#8553,2.);
#1381=VECTOR('',#8556,2.);
#1382=VECTOR('',#8559,2.);
#1383=VECTOR('',#8562,2.);
#1384=VECTOR('',#8565,2.);
#1385=VECTOR('',#8568,2.);
#1386=VECTOR('',#8571,2.);
#1387=VECTOR('',#8574,2.);
#1388=VECTOR('',#8577,2.);
#1389=VECTOR('',#8580,2.);
#1390=VECTOR('',#8583,1.5555);
#1391=VECTOR('',#8588,1.5555);
#1392=VECTOR('',#8591,1.5555);
#1393=VECTOR('',#8594,1.5555);
#1394=VECTOR('',#8597,1.5555);
#1395=VECTOR('',#8600,1.5555);
#1396=VECTOR('',#8603,1.5555);
#1397=VECTOR('',#8606,1.5555);
#1398=VECTOR('',#8609,1.5555);
#1399=VECTOR('',#8612,1.5555);
#1400=VECTOR('',#8615,1.5555);
#1401=VECTOR('',#8618,1.5555);
#1402=VECTOR('',#8621,1.5555);
#1403=VECTOR('',#8626,1.5);
#1404=VECTOR('',#8637,10.);
#1405=VECTOR('',#8638,10.);
#1406=VECTOR('',#8639,10.);
#1407=VECTOR('',#8640,10.);
#1408=VECTOR('',#8643,10.);
#1409=VECTOR('',#8644,10.);
#1410=VECTOR('',#8645,10.);
#1411=VECTOR('',#8648,10.);
#1412=VECTOR('',#8649,10.);
#1413=VECTOR('',#8650,10.);
#1414=VECTOR('',#8653,10.);
#1415=VECTOR('',#8654,10.);
#1416=VECTOR('',#8655,10.);
#1417=VECTOR('',#8658,10.);
#1418=VECTOR('',#8659,10.);
#1419=VECTOR('',#8660,10.);
#1420=VECTOR('',#8663,10.);
#1421=VECTOR('',#8664,10.);
#1422=VECTOR('',#8673,3.5);
#1587=CYLINDRICAL_SURFACE('',#7118,1.954);
#1588=CYLINDRICAL_SURFACE('',#7120,1.954);
#1589=CYLINDRICAL_SURFACE('',#7121,1.954);
#1590=CYLINDRICAL_SURFACE('',#7122,1.954);
#1591=CYLINDRICAL_SURFACE('',#7123,1.954);
#1592=CYLINDRICAL_SURFACE('',#7124,1.954);
#1593=CYLINDRICAL_SURFACE('',#7125,1.954);
#1594=CYLINDRICAL_SURFACE('',#7126,1.954);
#1595=CYLINDRICAL_SURFACE('',#7127,1.954);
#1596=CYLINDRICAL_SURFACE('',#7128,1.954);
#1597=CYLINDRICAL_SURFACE('',#7129,1.954);
#1598=CYLINDRICAL_SURFACE('',#7130,1.954);
#1599=CYLINDRICAL_SURFACE('',#7131,1.954);
#1600=CYLINDRICAL_SURFACE('',#7132,1.5555);
#1601=CYLINDRICAL_SURFACE('',#7134,1.5555);
#1602=CYLINDRICAL_SURFACE('',#7135,1.5555);
#1603=CYLINDRICAL_SURFACE('',#7136,1.5555);
#1604=CYLINDRICAL_SURFACE('',#7137,1.5555);
#1605=CYLINDRICAL_SURFACE('',#7138,1.5555);
#1606=CYLINDRICAL_SURFACE('',#7139,1.5555);
#1607=CYLINDRICAL_SURFACE('',#7140,1.5555);
#1608=CYLINDRICAL_SURFACE('',#7141,1.5555);
#1609=CYLINDRICAL_SURFACE('',#7142,1.5555);
#1610=CYLINDRICAL_SURFACE('',#7143,1.5555);
#1611=CYLINDRICAL_SURFACE('',#7144,1.5555);
#1612=CYLINDRICAL_SURFACE('',#7145,1.5555);
#1613=CYLINDRICAL_SURFACE('',#7149,1.5555);
#1614=CYLINDRICAL_SURFACE('',#7151,1.954);
#1615=CYLINDRICAL_SURFACE('',#7161,3.5);
#1685=FACE_BOUND('',#2469,.T.);
#1686=FACE_BOUND('',#2472,.T.);
#2003=FACE_OUTER_BOUND('',#2430,.T.);
#2004=FACE_OUTER_BOUND('',#2431,.T.);
#2005=FACE_OUTER_BOUND('',#2432,.T.);
#2006=FACE_OUTER_BOUND('',#2433,.T.);
#2007=FACE_OUTER_BOUND('',#2434,.T.);
#2008=FACE_OUTER_BOUND('',#2435,.T.);
#2009=FACE_OUTER_BOUND('',#2436,.T.);
#2010=FACE_OUTER_BOUND('',#2437,.T.);
#2011=FACE_OUTER_BOUND('',#2438,.T.);
#2012=FACE_OUTER_BOUND('',#2439,.T.);
#2013=FACE_OUTER_BOUND('',#2440,.T.);
#2014=FACE_OUTER_BOUND('',#2441,.T.);
#2015=FACE_OUTER_BOUND('',#2442,.T.);
#2016=FACE_OUTER_BOUND('',#2443,.T.);
#2017=FACE_OUTER_BOUND('',#2444,.T.);
#2018=FACE_OUTER_BOUND('',#2445,.T.);
#2019=FACE_OUTER_BOUND('',#2446,.T.);
#2020=FACE_OUTER_BOUND('',#2447,.T.);
#2021=FACE_OUTER_BOUND('',#2448,.T.);
#2022=FACE_OUTER_BOUND('',#2449,.T.);
#2023=FACE_OUTER_BOUND('',#2450,.T.);
#2024=FACE_OUTER_BOUND('',#2451,.T.);
#2025=FACE_OUTER_BOUND('',#2452,.T.);
#2026=FACE_OUTER_BOUND('',#2453,.T.);
#2027=FACE_OUTER_BOUND('',#2454,.T.);
#2028=FACE_OUTER_BOUND('',#2455,.T.);
#2029=FACE_OUTER_BOUND('',#2456,.T.);
#2030=FACE_OUTER_BOUND('',#2457,.T.);
#2031=FACE_OUTER_BOUND('',#2458,.T.);
#2032=FACE_OUTER_BOUND('',#2459,.T.);
#2033=FACE_OUTER_BOUND('',#2460,.T.);
#2034=FACE_OUTER_BOUND('',#2461,.T.);
#2035=FACE_OUTER_BOUND('',#2462,.T.);
#2036=FACE_OUTER_BOUND('',#2463,.T.);
#2037=FACE_OUTER_BOUND('',#2464,.T.);
#2038=FACE_OUTER_BOUND('',#2465,.T.);
#2039=FACE_OUTER_BOUND('',#2466,.T.);
#2040=FACE_OUTER_BOUND('',#2467,.T.);
#2041=FACE_OUTER_BOUND('',#2468,.T.);
#2042=FACE_OUTER_BOUND('',#2470,.T.);
#2043=FACE_OUTER_BOUND('',#2471,.T.);
#2044=FACE_OUTER_BOUND('',#2473,.T.);
#2430=EDGE_LOOP('',(#5685,#5686,#5687,#5688));
#2431=EDGE_LOOP('',(#5689,#5690,#5691,#5692));
#2432=EDGE_LOOP('',(#5693,#5694,#5695,#5696));
#2433=EDGE_LOOP('',(#5697,#5698,#5699,#5700));
#2434=EDGE_LOOP('',(#5701,#5702,#5703,#5704));
#2435=EDGE_LOOP('',(#5705,#5706,#5707,#5708));
#2436=EDGE_LOOP('',(#5709,#5710,#5711,#5712));
#2437=EDGE_LOOP('',(#5713,#5714,#5715,#5716));
#2438=EDGE_LOOP('',(#5717,#5718,#5719,#5720));
#2439=EDGE_LOOP('',(#5721,#5722,#5723,#5724));
#2440=EDGE_LOOP('',(#5725,#5726,#5727,#5728));
#2441=EDGE_LOOP('',(#5729,#5730,#5731,#5732));
#2442=EDGE_LOOP('',(#5733,#5734,#5735,#5736));
#2443=EDGE_LOOP('',(#5737,#5738,#5739,#5740));
#2444=EDGE_LOOP('',(#5741,#5742,#5743,#5744));
#2445=EDGE_LOOP('',(#5745,#5746,#5747,#5748));
#2446=EDGE_LOOP('',(#5749,#5750,#5751,#5752));
#2447=EDGE_LOOP('',(#5753,#5754,#5755,#5756));
#2448=EDGE_LOOP('',(#5757,#5758,#5759,#5760));
#2449=EDGE_LOOP('',(#5761,#5762,#5763,#5764));
#2450=EDGE_LOOP('',(#5765,#5766,#5767,#5768));
#2451=EDGE_LOOP('',(#5769,#5770,#5771,#5772));
#2452=EDGE_LOOP('',(#5773,#5774,#5775,#5776));
#2453=EDGE_LOOP('',(#5777,#5778,#5779,#5780));
#2454=EDGE_LOOP('',(#5781,#5782,#5783,#5784));
#2455=EDGE_LOOP('',(#5785,#5786,#5787,#5788));
#2456=EDGE_LOOP('',(#5789,#5790,#5791,#5792,#5793,#5794,#5795,#5796));
#2457=EDGE_LOOP('',(#5797,#5798,#5799,#5800,#5801,#5802,#5803,#5804,#5805,
#5806,#5807,#5808,#5809,#5810,#5811,#5812,#5813,#5814,#5815,#5816,#5817,
#5818,#5819,#5820,#5821,#5822,#5823,#5824,#5825,#5826));
#2458=EDGE_LOOP('',(#5827,#5828,#5829,#5830));
#2459=EDGE_LOOP('',(#5831,#5832,#5833,#5834,#5835,#5836,#5837,#5838,#5839,
#5840,#5841,#5842,#5843,#5844,#5845,#5846,#5847,#5848,#5849,#5850,#5851,
#5852,#5853,#5854,#5855,#5856,#5857,#5858,#5859,#5860,#5861));
#2460=EDGE_LOOP('',(#5862,#5863,#5864,#5865));
#2461=EDGE_LOOP('',(#5866,#5867,#5868,#5869));
#2462=EDGE_LOOP('',(#5870,#5871,#5872,#5873));
#2463=EDGE_LOOP('',(#5874,#5875,#5876,#5877));
#2464=EDGE_LOOP('',(#5878,#5879,#5880,#5881));
#2465=EDGE_LOOP('',(#5882,#5883,#5884,#5885));
#2466=EDGE_LOOP('',(#5886,#5887,#5888,#5889));
#2467=EDGE_LOOP('',(#5890,#5891,#5892,#5893,#5894,#5895));
#2468=EDGE_LOOP('',(#5896));
#2469=EDGE_LOOP('',(#5897,#5898,#5899,#5900));
#2470=EDGE_LOOP('',(#5901,#5902,#5903,#5904));
#2471=EDGE_LOOP('',(#5905));
#2472=EDGE_LOOP('',(#5906,#5907,#5908,#5909,#5910,#5911));
#2473=EDGE_LOOP('',(#5912));
#2611=CIRCLE('',#7119,1.954);
#2612=CIRCLE('',#7133,1.5555);
#2613=CIRCLE('',#7147,1.954);
#2614=CIRCLE('',#7148,1.);
#2615=CIRCLE('',#7150,1.5555);
#2616=CIRCLE('',#7160,3.5);
#2617=CIRCLE('',#7162,3.5);
#3140=VERTEX_POINT('',#17589);
#3141=VERTEX_POINT('',#17590);
#3142=VERTEX_POINT('',#17592);
#3143=VERTEX_POINT('',#17603);
#3144=VERTEX_POINT('',#17613);
#3145=VERTEX_POINT('',#17614);
#3146=VERTEX_POINT('',#17661);
#3147=VERTEX_POINT('',#17662);
#3148=VERTEX_POINT('',#17709);
#3149=VERTEX_POINT('',#17710);
#3150=VERTEX_POINT('',#17760);
#3151=VERTEX_POINT('',#17761);
#3152=VERTEX_POINT('',#17808);
#3153=VERTEX_POINT('',#17809);
#3154=VERTEX_POINT('',#17856);
#3155=VERTEX_POINT('',#17857);
#3156=VERTEX_POINT('',#17904);
#3157=VERTEX_POINT('',#17905);
#3158=VERTEX_POINT('',#17958);
#3159=VERTEX_POINT('',#17959);
#3160=VERTEX_POINT('',#18006);
#3161=VERTEX_POINT('',#18007);
#3162=VERTEX_POINT('',#18054);
#3163=VERTEX_POINT('',#18055);
#3164=VERTEX_POINT('',#18108);
#3165=VERTEX_POINT('',#18109);
#3166=VERTEX_POINT('',#18156);
#3167=VERTEX_POINT('',#18157);
#3168=VERTEX_POINT('',#18204);
#3169=VERTEX_POINT('',#18205);
#3170=VERTEX_POINT('',#18207);
#3171=VERTEX_POINT('',#18217);
#3172=VERTEX_POINT('',#18228);
#3173=VERTEX_POINT('',#18229);
#3174=VERTEX_POINT('',#18252);
#3175=VERTEX_POINT('',#18253);
#3176=VERTEX_POINT('',#18276);
#3177=VERTEX_POINT('',#18277);
#3178=VERTEX_POINT('',#18301);
#3179=VERTEX_POINT('',#18302);
#3180=VERTEX_POINT('',#18326);
#3181=VERTEX_POINT('',#18327);
#3182=VERTEX_POINT('',#18350);
#3183=VERTEX_POINT('',#18351);
#3184=VERTEX_POINT('',#18375);
#3185=VERTEX_POINT('',#18376);
#3186=VERTEX_POINT('',#18400);
#3187=VERTEX_POINT('',#18401);
#3188=VERTEX_POINT('',#18424);
#3189=VERTEX_POINT('',#18425);
#3190=VERTEX_POINT('',#18448);
#3191=VERTEX_POINT('',#18449);
#3192=VERTEX_POINT('',#18473);
#3193=VERTEX_POINT('',#18474);
#3194=VERTEX_POINT('',#18498);
#3195=VERTEX_POINT('',#18499);
#3196=VERTEX_POINT('',#18522);
#3197=VERTEX_POINT('',#18686);
#3198=VERTEX_POINT('',#18745);
#3199=VERTEX_POINT('',#18811);
#3200=VERTEX_POINT('',#19166);
#3201=VERTEX_POINT('',#19277);
#3202=VERTEX_POINT('',#19751);
#3203=VERTEX_POINT('',#19752);
#3204=VERTEX_POINT('',#19754);
#3205=VERTEX_POINT('',#19756);
#3206=VERTEX_POINT('',#19760);
#3207=VERTEX_POINT('',#19762);
#3208=VERTEX_POINT('',#19766);
#3209=VERTEX_POINT('',#19768);
#3210=VERTEX_POINT('',#19772);
#3211=VERTEX_POINT('',#19774);
#3212=VERTEX_POINT('',#19778);
#3213=VERTEX_POINT('',#19780);
#3214=VERTEX_POINT('',#19788);
#3215=VERTEX_POINT('',#19791);
#4001=EDGE_CURVE('',#3140,#3141,#912,.T.);
#4002=EDGE_CURVE('',#3140,#3142,#356,.T.);
#4003=EDGE_CURVE('',#3142,#3143,#2611,.F.);
#4004=EDGE_CURVE('',#3143,#3141,#357,.T.);
#4005=EDGE_CURVE('',#3144,#3145,#913,.T.);
#4006=EDGE_CURVE('',#3144,#3140,#358,.T.);
#4007=EDGE_CURVE('',#3141,#3145,#359,.T.);
#4008=EDGE_CURVE('',#3146,#3147,#914,.T.);
#4009=EDGE_CURVE('',#3146,#3144,#360,.T.);
#4010=EDGE_CURVE('',#3145,#3147,#361,.T.);
#4011=EDGE_CURVE('',#3148,#3149,#915,.T.);
#4012=EDGE_CURVE('',#3148,#3146,#362,.T.);
#4013=EDGE_CURVE('',#3147,#3149,#363,.T.);
#4014=EDGE_CURVE('',#3150,#3151,#916,.T.);
#4015=EDGE_CURVE('',#3150,#3148,#364,.T.);
#4016=EDGE_CURVE('',#3149,#3151,#365,.T.);
#4017=EDGE_CURVE('',#3152,#3153,#917,.T.);
#4018=EDGE_CURVE('',#3152,#3150,#366,.T.);
#4019=EDGE_CURVE('',#3151,#3153,#367,.T.);
#4020=EDGE_CURVE('',#3154,#3155,#918,.T.);
#4021=EDGE_CURVE('',#3154,#3152,#368,.T.);
#4022=EDGE_CURVE('',#3153,#3155,#369,.T.);
#4023=EDGE_CURVE('',#3156,#3157,#919,.T.);
#4024=EDGE_CURVE('',#3156,#3154,#370,.T.);
#4025=EDGE_CURVE('',#3155,#3157,#371,.T.);
#4026=EDGE_CURVE('',#3158,#3159,#920,.T.);
#4027=EDGE_CURVE('',#3158,#3156,#372,.T.);
#4028=EDGE_CURVE('',#3157,#3159,#373,.T.);
#4029=EDGE_CURVE('',#3160,#3161,#921,.T.);
#4030=EDGE_CURVE('',#3160,#3158,#374,.T.);
#4031=EDGE_CURVE('',#3159,#3161,#375,.T.);
#4032=EDGE_CURVE('',#3162,#3163,#922,.T.);
#4033=EDGE_CURVE('',#3162,#3160,#376,.T.);
#4034=EDGE_CURVE('',#3161,#3163,#377,.T.);
#4035=EDGE_CURVE('',#3164,#3165,#923,.T.);
#4036=EDGE_CURVE('',#3164,#3162,#378,.T.);
#4037=EDGE_CURVE('',#3163,#3165,#379,.T.);
#4038=EDGE_CURVE('',#3166,#3167,#924,.T.);
#4039=EDGE_CURVE('',#3166,#3164,#380,.T.);
#4040=EDGE_CURVE('',#3165,#3167,#381,.T.);
#4041=EDGE_CURVE('',#3168,#3169,#925,.T.);
#4042=EDGE_CURVE('',#3168,#3170,#382,.T.);
#4043=EDGE_CURVE('',#3170,#3171,#2612,.T.);
#4044=EDGE_CURVE('',#3169,#3171,#383,.T.);
#4045=EDGE_CURVE('',#3172,#3173,#926,.T.);
#4046=EDGE_CURVE('',#3172,#3168,#384,.T.);
#4047=EDGE_CURVE('',#3173,#3169,#385,.T.);
#4048=EDGE_CURVE('',#3174,#3175,#927,.T.);
#4049=EDGE_CURVE('',#3174,#3172,#386,.T.);
#4050=EDGE_CURVE('',#3175,#3173,#387,.T.);
#4051=EDGE_CURVE('',#3176,#3177,#928,.T.);
#4052=EDGE_CURVE('',#3176,#3174,#388,.T.);
#4053=EDGE_CURVE('',#3177,#3175,#389,.T.);
#4054=EDGE_CURVE('',#3178,#3179,#929,.T.);
#4055=EDGE_CURVE('',#3178,#3176,#390,.T.);
#4056=EDGE_CURVE('',#3179,#3177,#391,.T.);
#4057=EDGE_CURVE('',#3180,#3181,#930,.T.);
#4058=EDGE_CURVE('',#3180,#3178,#392,.T.);
#4059=EDGE_CURVE('',#3181,#3179,#393,.T.);
#4060=EDGE_CURVE('',#3182,#3183,#931,.T.);
#4061=EDGE_CURVE('',#3182,#3180,#394,.T.);
#4062=EDGE_CURVE('',#3183,#3181,#395,.T.);
#4063=EDGE_CURVE('',#3184,#3185,#932,.T.);
#4064=EDGE_CURVE('',#3184,#3182,#396,.T.);
#4065=EDGE_CURVE('',#3185,#3183,#397,.T.);
#4066=EDGE_CURVE('',#3186,#3187,#933,.T.);
#4067=EDGE_CURVE('',#3186,#3184,#398,.T.);
#4068=EDGE_CURVE('',#3187,#3185,#399,.T.);
#4069=EDGE_CURVE('',#3188,#3189,#934,.T.);
#4070=EDGE_CURVE('',#3188,#3186,#400,.T.);
#4071=EDGE_CURVE('',#3189,#3187,#401,.T.);
#4072=EDGE_CURVE('',#3190,#3191,#935,.T.);
#4073=EDGE_CURVE('',#3190,#3188,#402,.T.);
#4074=EDGE_CURVE('',#3191,#3189,#403,.T.);
#4075=EDGE_CURVE('',#3192,#3193,#936,.T.);
#4076=EDGE_CURVE('',#3192,#3190,#404,.T.);
#4077=EDGE_CURVE('',#3193,#3191,#405,.T.);
#4078=EDGE_CURVE('',#3194,#3195,#937,.T.);
#4079=EDGE_CURVE('',#3194,#3192,#406,.T.);
#4080=EDGE_CURVE('',#3195,#3193,#407,.T.);
#4081=EDGE_CURVE('',#3171,#3196,#408,.T.);
#4082=EDGE_CURVE('',#3197,#3170,#409,.T.);
#4083=EDGE_CURVE('',#3198,#3197,#2613,.T.);
#4084=EDGE_CURVE('',#3196,#3198,#410,.T.);
#4085=EDGE_CURVE('',#3196,#3199,#938,.T.);
#4086=EDGE_CURVE('',#3199,#3199,#2614,.T.);
#4087=EDGE_CURVE('',#3200,#3194,#411,.T.);
#4088=EDGE_CURVE('',#3142,#3200,#412,.T.);
#4089=EDGE_CURVE('',#3197,#3166,#413,.T.);
#4090=EDGE_CURVE('',#3201,#3195,#414,.T.);
#4091=EDGE_CURVE('',#3200,#3201,#2615,.T.);
#4092=EDGE_CURVE('',#3167,#3198,#415,.T.);
#4093=EDGE_CURVE('',#3201,#3143,#416,.T.);
#4094=EDGE_CURVE('',#3202,#3203,#939,.T.);
#4095=EDGE_CURVE('',#3202,#3204,#940,.T.);
#4096=EDGE_CURVE('',#3204,#3205,#941,.T.);
#4097=EDGE_CURVE('',#3203,#3205,#942,.T.);
#4098=EDGE_CURVE('',#3206,#3202,#943,.T.);
#4099=EDGE_CURVE('',#3206,#3207,#944,.T.);
#4100=EDGE_CURVE('',#3207,#3204,#945,.T.);
#4101=EDGE_CURVE('',#3208,#3206,#946,.T.);
#4102=EDGE_CURVE('',#3208,#3209,#947,.T.);
#4103=EDGE_CURVE('',#3209,#3207,#948,.T.);
#4104=EDGE_CURVE('',#3210,#3208,#949,.T.);
#4105=EDGE_CURVE('',#3210,#3211,#950,.T.);
#4106=EDGE_CURVE('',#3211,#3209,#951,.T.);
#4107=EDGE_CURVE('',#3212,#3210,#952,.T.);
#4108=EDGE_CURVE('',#3212,#3213,#953,.T.);
#4109=EDGE_CURVE('',#3213,#3211,#954,.T.);
#4110=EDGE_CURVE('',#3203,#3212,#955,.T.);
#4111=EDGE_CURVE('',#3205,#3213,#956,.T.);
#4112=EDGE_CURVE('',#3214,#3214,#2616,.T.);
#4113=EDGE_CURVE('',#3214,#3215,#957,.T.);
#4114=EDGE_CURVE('',#3215,#3215,#2617,.T.);
#5685=ORIENTED_EDGE('',*,*,#4001,.F.);
#5686=ORIENTED_EDGE('',*,*,#4002,.T.);
#5687=ORIENTED_EDGE('',*,*,#4003,.T.);
#5688=ORIENTED_EDGE('',*,*,#4004,.T.);
#5689=ORIENTED_EDGE('',*,*,#4005,.F.);
#5690=ORIENTED_EDGE('',*,*,#4006,.T.);
#5691=ORIENTED_EDGE('',*,*,#4001,.T.);
#5692=ORIENTED_EDGE('',*,*,#4007,.T.);
#5693=ORIENTED_EDGE('',*,*,#4008,.F.);
#5694=ORIENTED_EDGE('',*,*,#4009,.T.);
#5695=ORIENTED_EDGE('',*,*,#4005,.T.);
#5696=ORIENTED_EDGE('',*,*,#4010,.T.);
#5697=ORIENTED_EDGE('',*,*,#4011,.F.);
#5698=ORIENTED_EDGE('',*,*,#4012,.T.);
#5699=ORIENTED_EDGE('',*,*,#4008,.T.);
#5700=ORIENTED_EDGE('',*,*,#4013,.T.);
#5701=ORIENTED_EDGE('',*,*,#4014,.F.);
#5702=ORIENTED_EDGE('',*,*,#4015,.T.);
#5703=ORIENTED_EDGE('',*,*,#4011,.T.);
#5704=ORIENTED_EDGE('',*,*,#4016,.T.);
#5705=ORIENTED_EDGE('',*,*,#4017,.F.);
#5706=ORIENTED_EDGE('',*,*,#4018,.T.);
#5707=ORIENTED_EDGE('',*,*,#4014,.T.);
#5708=ORIENTED_EDGE('',*,*,#4019,.T.);
#5709=ORIENTED_EDGE('',*,*,#4020,.F.);
#5710=ORIENTED_EDGE('',*,*,#4021,.T.);
#5711=ORIENTED_EDGE('',*,*,#4017,.T.);
#5712=ORIENTED_EDGE('',*,*,#4022,.T.);
#5713=ORIENTED_EDGE('',*,*,#4023,.F.);
#5714=ORIENTED_EDGE('',*,*,#4024,.T.);
#5715=ORIENTED_EDGE('',*,*,#4020,.T.);
#5716=ORIENTED_EDGE('',*,*,#4025,.T.);
#5717=ORIENTED_EDGE('',*,*,#4026,.F.);
#5718=ORIENTED_EDGE('',*,*,#4027,.T.);
#5719=ORIENTED_EDGE('',*,*,#4023,.T.);
#5720=ORIENTED_EDGE('',*,*,#4028,.T.);
#5721=ORIENTED_EDGE('',*,*,#4029,.F.);
#5722=ORIENTED_EDGE('',*,*,#4030,.T.);
#5723=ORIENTED_EDGE('',*,*,#4026,.T.);
#5724=ORIENTED_EDGE('',*,*,#4031,.T.);
#5725=ORIENTED_EDGE('',*,*,#4032,.F.);
#5726=ORIENTED_EDGE('',*,*,#4033,.T.);
#5727=ORIENTED_EDGE('',*,*,#4029,.T.);
#5728=ORIENTED_EDGE('',*,*,#4034,.T.);
#5729=ORIENTED_EDGE('',*,*,#4035,.F.);
#5730=ORIENTED_EDGE('',*,*,#4036,.T.);
#5731=ORIENTED_EDGE('',*,*,#4032,.T.);
#5732=ORIENTED_EDGE('',*,*,#4037,.T.);
#5733=ORIENTED_EDGE('',*,*,#4038,.F.);
#5734=ORIENTED_EDGE('',*,*,#4039,.T.);
#5735=ORIENTED_EDGE('',*,*,#4035,.T.);
#5736=ORIENTED_EDGE('',*,*,#4040,.T.);
#5737=ORIENTED_EDGE('',*,*,#4041,.F.);
#5738=ORIENTED_EDGE('',*,*,#4042,.T.);
#5739=ORIENTED_EDGE('',*,*,#4043,.T.);
#5740=ORIENTED_EDGE('',*,*,#4044,.F.);
#5741=ORIENTED_EDGE('',*,*,#4045,.F.);
#5742=ORIENTED_EDGE('',*,*,#4046,.T.);
#5743=ORIENTED_EDGE('',*,*,#4041,.T.);
#5744=ORIENTED_EDGE('',*,*,#4047,.F.);
#5745=ORIENTED_EDGE('',*,*,#4048,.F.);
#5746=ORIENTED_EDGE('',*,*,#4049,.T.);
#5747=ORIENTED_EDGE('',*,*,#4045,.T.);
#5748=ORIENTED_EDGE('',*,*,#4050,.F.);
#5749=ORIENTED_EDGE('',*,*,#4051,.F.);
#5750=ORIENTED_EDGE('',*,*,#4052,.T.);
#5751=ORIENTED_EDGE('',*,*,#4048,.T.);
#5752=ORIENTED_EDGE('',*,*,#4053,.F.);
#5753=ORIENTED_EDGE('',*,*,#4054,.F.);
#5754=ORIENTED_EDGE('',*,*,#4055,.T.);
#5755=ORIENTED_EDGE('',*,*,#4051,.T.);
#5756=ORIENTED_EDGE('',*,*,#4056,.F.);
#5757=ORIENTED_EDGE('',*,*,#4057,.F.);
#5758=ORIENTED_EDGE('',*,*,#4058,.T.);
#5759=ORIENTED_EDGE('',*,*,#4054,.T.);
#5760=ORIENTED_EDGE('',*,*,#4059,.F.);
#5761=ORIENTED_EDGE('',*,*,#4060,.F.);
#5762=ORIENTED_EDGE('',*,*,#4061,.T.);
#5763=ORIENTED_EDGE('',*,*,#4057,.T.);
#5764=ORIENTED_EDGE('',*,*,#4062,.F.);
#5765=ORIENTED_EDGE('',*,*,#4063,.F.);
#5766=ORIENTED_EDGE('',*,*,#4064,.T.);
#5767=ORIENTED_EDGE('',*,*,#4060,.T.);
#5768=ORIENTED_EDGE('',*,*,#4065,.F.);
#5769=ORIENTED_EDGE('',*,*,#4066,.F.);
#5770=ORIENTED_EDGE('',*,*,#4067,.T.);
#5771=ORIENTED_EDGE('',*,*,#4063,.T.);
#5772=ORIENTED_EDGE('',*,*,#4068,.F.);
#5773=ORIENTED_EDGE('',*,*,#4069,.F.);
#5774=ORIENTED_EDGE('',*,*,#4070,.T.);
#5775=ORIENTED_EDGE('',*,*,#4066,.T.);
#5776=ORIENTED_EDGE('',*,*,#4071,.F.);
#5777=ORIENTED_EDGE('',*,*,#4072,.F.);
#5778=ORIENTED_EDGE('',*,*,#4073,.T.);
#5779=ORIENTED_EDGE('',*,*,#4069,.T.);
#5780=ORIENTED_EDGE('',*,*,#4074,.F.);
#5781=ORIENTED_EDGE('',*,*,#4075,.F.);
#5782=ORIENTED_EDGE('',*,*,#4076,.T.);
#5783=ORIENTED_EDGE('',*,*,#4072,.T.);
#5784=ORIENTED_EDGE('',*,*,#4077,.F.);
#5785=ORIENTED_EDGE('',*,*,#4078,.F.);
#5786=ORIENTED_EDGE('',*,*,#4079,.T.);
#5787=ORIENTED_EDGE('',*,*,#4075,.T.);
#5788=ORIENTED_EDGE('',*,*,#4080,.F.);
#5789=ORIENTED_EDGE('',*,*,#4081,.F.);
#5790=ORIENTED_EDGE('',*,*,#4043,.F.);
#5791=ORIENTED_EDGE('',*,*,#4082,.F.);
#5792=ORIENTED_EDGE('',*,*,#4083,.F.);
#5793=ORIENTED_EDGE('',*,*,#4084,.F.);
#5794=ORIENTED_EDGE('',*,*,#4085,.T.);
#5795=ORIENTED_EDGE('',*,*,#4086,.F.);
#5796=ORIENTED_EDGE('',*,*,#4085,.F.);
#5797=ORIENTED_EDGE('',*,*,#4082,.T.);
#5798=ORIENTED_EDGE('',*,*,#4042,.F.);
#5799=ORIENTED_EDGE('',*,*,#4046,.F.);
#5800=ORIENTED_EDGE('',*,*,#4049,.F.);
#5801=ORIENTED_EDGE('',*,*,#4052,.F.);
#5802=ORIENTED_EDGE('',*,*,#4055,.F.);
#5803=ORIENTED_EDGE('',*,*,#4058,.F.);
#5804=ORIENTED_EDGE('',*,*,#4061,.F.);
#5805=ORIENTED_EDGE('',*,*,#4064,.F.);
#5806=ORIENTED_EDGE('',*,*,#4067,.F.);
#5807=ORIENTED_EDGE('',*,*,#4070,.F.);
#5808=ORIENTED_EDGE('',*,*,#4073,.F.);
#5809=ORIENTED_EDGE('',*,*,#4076,.F.);
#5810=ORIENTED_EDGE('',*,*,#4079,.F.);
#5811=ORIENTED_EDGE('',*,*,#4087,.F.);
#5812=ORIENTED_EDGE('',*,*,#4088,.F.);
#5813=ORIENTED_EDGE('',*,*,#4002,.F.);
#5814=ORIENTED_EDGE('',*,*,#4006,.F.);
#5815=ORIENTED_EDGE('',*,*,#4009,.F.);
#5816=ORIENTED_EDGE('',*,*,#4012,.F.);
#5817=ORIENTED_EDGE('',*,*,#4015,.F.);
#5818=ORIENTED_EDGE('',*,*,#4018,.F.);
#5819=ORIENTED_EDGE('',*,*,#4021,.F.);
#5820=ORIENTED_EDGE('',*,*,#4024,.F.);
#5821=ORIENTED_EDGE('',*,*,#4027,.F.);
#5822=ORIENTED_EDGE('',*,*,#4030,.F.);
#5823=ORIENTED_EDGE('',*,*,#4033,.F.);
#5824=ORIENTED_EDGE('',*,*,#4036,.F.);
#5825=ORIENTED_EDGE('',*,*,#4039,.F.);
#5826=ORIENTED_EDGE('',*,*,#4089,.F.);
#5827=ORIENTED_EDGE('',*,*,#4078,.T.);
#5828=ORIENTED_EDGE('',*,*,#4090,.F.);
#5829=ORIENTED_EDGE('',*,*,#4091,.F.);
#5830=ORIENTED_EDGE('',*,*,#4087,.T.);
#5831=ORIENTED_EDGE('',*,*,#4081,.T.);
#5832=ORIENTED_EDGE('',*,*,#4084,.T.);
#5833=ORIENTED_EDGE('',*,*,#4092,.F.);
#5834=ORIENTED_EDGE('',*,*,#4040,.F.);
#5835=ORIENTED_EDGE('',*,*,#4037,.F.);
#5836=ORIENTED_EDGE('',*,*,#4034,.F.);
#5837=ORIENTED_EDGE('',*,*,#4031,.F.);
#5838=ORIENTED_EDGE('',*,*,#4028,.F.);
#5839=ORIENTED_EDGE('',*,*,#4025,.F.);
#5840=ORIENTED_EDGE('',*,*,#4022,.F.);
#5841=ORIENTED_EDGE('',*,*,#4019,.F.);
#5842=ORIENTED_EDGE('',*,*,#4016,.F.);
#5843=ORIENTED_EDGE('',*,*,#4013,.F.);
#5844=ORIENTED_EDGE('',*,*,#4010,.F.);
#5845=ORIENTED_EDGE('',*,*,#4007,.F.);
#5846=ORIENTED_EDGE('',*,*,#4004,.F.);
#5847=ORIENTED_EDGE('',*,*,#4093,.F.);
#5848=ORIENTED_EDGE('',*,*,#4090,.T.);
#5849=ORIENTED_EDGE('',*,*,#4080,.T.);
#5850=ORIENTED_EDGE('',*,*,#4077,.T.);
#5851=ORIENTED_EDGE('',*,*,#4074,.T.);
#5852=ORIENTED_EDGE('',*,*,#4071,.T.);
#5853=ORIENTED_EDGE('',*,*,#4068,.T.);
#5854=ORIENTED_EDGE('',*,*,#4065,.T.);
#5855=ORIENTED_EDGE('',*,*,#4062,.T.);
#5856=ORIENTED_EDGE('',*,*,#4059,.T.);
#5857=ORIENTED_EDGE('',*,*,#4056,.T.);
#5858=ORIENTED_EDGE('',*,*,#4053,.T.);
#5859=ORIENTED_EDGE('',*,*,#4050,.T.);
#5860=ORIENTED_EDGE('',*,*,#4047,.T.);
#5861=ORIENTED_EDGE('',*,*,#4044,.T.);
#5862=ORIENTED_EDGE('',*,*,#4038,.T.);
#5863=ORIENTED_EDGE('',*,*,#4092,.T.);
#5864=ORIENTED_EDGE('',*,*,#4083,.T.);
#5865=ORIENTED_EDGE('',*,*,#4089,.T.);
#5866=ORIENTED_EDGE('',*,*,#4094,.F.);
#5867=ORIENTED_EDGE('',*,*,#4095,.T.);
#5868=ORIENTED_EDGE('',*,*,#4096,.T.);
#5869=ORIENTED_EDGE('',*,*,#4097,.F.);
#5870=ORIENTED_EDGE('',*,*,#4098,.F.);
#5871=ORIENTED_EDGE('',*,*,#4099,.T.);
#5872=ORIENTED_EDGE('',*,*,#4100,.T.);
#5873=ORIENTED_EDGE('',*,*,#4095,.F.);
#5874=ORIENTED_EDGE('',*,*,#4101,.F.);
#5875=ORIENTED_EDGE('',*,*,#4102,.T.);
#5876=ORIENTED_EDGE('',*,*,#4103,.T.);
#5877=ORIENTED_EDGE('',*,*,#4099,.F.);
#5878=ORIENTED_EDGE('',*,*,#4104,.F.);
#5879=ORIENTED_EDGE('',*,*,#4105,.T.);
#5880=ORIENTED_EDGE('',*,*,#4106,.T.);
#5881=ORIENTED_EDGE('',*,*,#4102,.F.);
#5882=ORIENTED_EDGE('',*,*,#4107,.F.);
#5883=ORIENTED_EDGE('',*,*,#4108,.T.);
#5884=ORIENTED_EDGE('',*,*,#4109,.T.);
#5885=ORIENTED_EDGE('',*,*,#4105,.F.);
#5886=ORIENTED_EDGE('',*,*,#4110,.F.);
#5887=ORIENTED_EDGE('',*,*,#4097,.T.);
#5888=ORIENTED_EDGE('',*,*,#4111,.T.);
#5889=ORIENTED_EDGE('',*,*,#4108,.F.);
#5890=ORIENTED_EDGE('',*,*,#4111,.F.);
#5891=ORIENTED_EDGE('',*,*,#4096,.F.);
#5892=ORIENTED_EDGE('',*,*,#4100,.F.);
#5893=ORIENTED_EDGE('',*,*,#4103,.F.);
#5894=ORIENTED_EDGE('',*,*,#4106,.F.);
#5895=ORIENTED_EDGE('',*,*,#4109,.F.);
#5896=ORIENTED_EDGE('',*,*,#4112,.T.);
#5897=ORIENTED_EDGE('',*,*,#4088,.T.);
#5898=ORIENTED_EDGE('',*,*,#4091,.T.);
#5899=ORIENTED_EDGE('',*,*,#4093,.T.);
#5900=ORIENTED_EDGE('',*,*,#4003,.F.);
#5901=ORIENTED_EDGE('',*,*,#4112,.F.);
#5902=ORIENTED_EDGE('',*,*,#4113,.T.);
#5903=ORIENTED_EDGE('',*,*,#4114,.T.);
#5904=ORIENTED_EDGE('',*,*,#4113,.F.);
#5905=ORIENTED_EDGE('',*,*,#4114,.F.);
#5906=ORIENTED_EDGE('',*,*,#4094,.T.);
#5907=ORIENTED_EDGE('',*,*,#4110,.T.);
#5908=ORIENTED_EDGE('',*,*,#4107,.T.);
#5909=ORIENTED_EDGE('',*,*,#4104,.T.);
#5910=ORIENTED_EDGE('',*,*,#4101,.T.);
#5911=ORIENTED_EDGE('',*,*,#4098,.T.);
#5912=ORIENTED_EDGE('',*,*,#4086,.T.);
#6056=PLANE('',#7152);
#6057=PLANE('',#7153);
#6058=PLANE('',#7154);
#6059=PLANE('',#7155);
#6060=PLANE('',#7156);
#6061=PLANE('',#7157);
#6062=PLANE('',#7158);
#6063=PLANE('',#7159);
#6064=PLANE('',#7163);
#6065=PLANE('',#7164);
#6382=ADVANCED_FACE('',(#2003),#1587,.T.);
#6383=ADVANCED_FACE('',(#2004),#1588,.T.);
#6384=ADVANCED_FACE('',(#2005),#1589,.T.);
#6385=ADVANCED_FACE('',(#2006),#1590,.T.);
#6386=ADVANCED_FACE('',(#2007),#1591,.T.);
#6387=ADVANCED_FACE('',(#2008),#1592,.T.);
#6388=ADVANCED_FACE('',(#2009),#1593,.T.);
#6389=ADVANCED_FACE('',(#2010),#1594,.T.);
#6390=ADVANCED_FACE('',(#2011),#1595,.T.);
#6391=ADVANCED_FACE('',(#2012),#1596,.T.);
#6392=ADVANCED_FACE('',(#2013),#1597,.T.);
#6393=ADVANCED_FACE('',(#2014),#1598,.T.);
#6394=ADVANCED_FACE('',(#2015),#1599,.T.);
#6395=ADVANCED_FACE('',(#2016),#1600,.T.);
#6396=ADVANCED_FACE('',(#2017),#1601,.T.);
#6397=ADVANCED_FACE('',(#2018),#1602,.T.);
#6398=ADVANCED_FACE('',(#2019),#1603,.T.);
#6399=ADVANCED_FACE('',(#2020),#1604,.T.);
#6400=ADVANCED_FACE('',(#2021),#1605,.T.);
#6401=ADVANCED_FACE('',(#2022),#1606,.T.);
#6402=ADVANCED_FACE('',(#2023),#1607,.T.);
#6403=ADVANCED_FACE('',(#2024),#1608,.T.);
#6404=ADVANCED_FACE('',(#2025),#1609,.T.);
#6405=ADVANCED_FACE('',(#2026),#1610,.T.);
#6406=ADVANCED_FACE('',(#2027),#1611,.T.);
#6407=ADVANCED_FACE('',(#2028),#1612,.T.);
#6408=ADVANCED_FACE('',(#2029),#116,.T.);
#6409=ADVANCED_FACE('',(#2030),#125,.F.);
#6410=ADVANCED_FACE('',(#2031),#1613,.T.);
#6411=ADVANCED_FACE('',(#2032),#126,.F.);
#6412=ADVANCED_FACE('',(#2033),#1614,.T.);
#6413=ADVANCED_FACE('',(#2034),#6056,.F.);
#6414=ADVANCED_FACE('',(#2035),#6057,.F.);
#6415=ADVANCED_FACE('',(#2036),#6058,.F.);
#6416=ADVANCED_FACE('',(#2037),#6059,.F.);
#6417=ADVANCED_FACE('',(#2038),#6060,.F.);
#6418=ADVANCED_FACE('',(#2039),#6061,.F.);
#6419=ADVANCED_FACE('',(#2040),#6062,.F.);
#6420=ADVANCED_FACE('',(#2041,#1685),#6063,.T.);
#6421=ADVANCED_FACE('',(#2042),#1615,.T.);
#6422=ADVANCED_FACE('',(#2043,#1686),#6064,.F.);
#6423=ADVANCED_FACE('',(#2044),#6065,.T.);
#6442=CLOSED_SHELL('',(#6382,#6383,#6384,#6385,#6386,#6387,#6388,#6389,
#6390,#6391,#6392,#6393,#6394,#6395,#6396,#6397,#6398,#6399,#6400,#6401,
#6402,#6403,#6404,#6405,#6406,#6407,#6408,#6409,#6410,#6411,#6412,#6413,
#6414,#6415,#6416,#6417,#6418,#6419,#6420,#6421,#6422,#6423));
#7117=AXIS2_PLACEMENT_3D('',#17587,#8538,#8539);
#7118=AXIS2_PLACEMENT_3D('',#17588,#8540,#8541);
#7119=AXIS2_PLACEMENT_3D('',#17604,#8543,#8544);
#7120=AXIS2_PLACEMENT_3D('',#17612,#8545,#8546);
#7121=AXIS2_PLACEMENT_3D('',#17660,#8548,#8549);
#7122=AXIS2_PLACEMENT_3D('',#17708,#8551,#8552);
#7123=AXIS2_PLACEMENT_3D('',#17759,#8554,#8555);
#7124=AXIS2_PLACEMENT_3D('',#17807,#8557,#8558);
#7125=AXIS2_PLACEMENT_3D('',#17855,#8560,#8561);
#7126=AXIS2_PLACEMENT_3D('',#17903,#8563,#8564);
#7127=AXIS2_PLACEMENT_3D('',#17957,#8566,#8567);
#7128=AXIS2_PLACEMENT_3D('',#18005,#8569,#8570);
#7129=AXIS2_PLACEMENT_3D('',#18053,#8572,#8573);
#7130=AXIS2_PLACEMENT_3D('',#18107,#8575,#8576);
#7131=AXIS2_PLACEMENT_3D('',#18155,#8578,#8579);
#7132=AXIS2_PLACEMENT_3D('',#18203,#8581,#8582);
#7133=AXIS2_PLACEMENT_3D('',#18218,#8584,#8585);
#7134=AXIS2_PLACEMENT_3D('',#18227,#8586,#8587);
#7135=AXIS2_PLACEMENT_3D('',#18251,#8589,#8590);
#7136=AXIS2_PLACEMENT_3D('',#18275,#8592,#8593);
#7137=AXIS2_PLACEMENT_3D('',#18300,#8595,#8596);
#7138=AXIS2_PLACEMENT_3D('',#18325,#8598,#8599);
#7139=AXIS2_PLACEMENT_3D('',#18349,#8601,#8602);
#7140=AXIS2_PLACEMENT_3D('',#18374,#8604,#8605);
#7141=AXIS2_PLACEMENT_3D('',#18399,#8607,#8608);
#7142=AXIS2_PLACEMENT_3D('',#18423,#8610,#8611);
#7143=AXIS2_PLACEMENT_3D('',#18447,#8613,#8614);
#7144=AXIS2_PLACEMENT_3D('',#18472,#8616,#8617);
#7145=AXIS2_PLACEMENT_3D('',#18497,#8619,#8620);
#7146=AXIS2_PLACEMENT_3D('',#18521,#8622,#8623);
#7147=AXIS2_PLACEMENT_3D('',#18746,#8624,#8625);
#7148=AXIS2_PLACEMENT_3D('',#18813,#8627,#8628);
#7149=AXIS2_PLACEMENT_3D('',#19276,#8629,#8630);
#7150=AXIS2_PLACEMENT_3D('',#19287,#8631,#8632);
#7151=AXIS2_PLACEMENT_3D('',#19749,#8633,#8634);
#7152=AXIS2_PLACEMENT_3D('',#19750,#8635,#8636);
#7153=AXIS2_PLACEMENT_3D('',#19759,#8641,#8642);
#7154=AXIS2_PLACEMENT_3D('',#19765,#8646,#8647);
#7155=AXIS2_PLACEMENT_3D('',#19771,#8651,#8652);
#7156=AXIS2_PLACEMENT_3D('',#19777,#8656,#8657);
#7157=AXIS2_PLACEMENT_3D('',#19783,#8661,#8662);
#7158=AXIS2_PLACEMENT_3D('',#19786,#8665,#8666);
#7159=AXIS2_PLACEMENT_3D('',#19787,#8667,#8668);
#7160=AXIS2_PLACEMENT_3D('',#19789,#8669,#8670);
#7161=AXIS2_PLACEMENT_3D('',#19790,#8671,#8672);
#7162=AXIS2_PLACEMENT_3D('',#19793,#8674,#8675);
#7163=AXIS2_PLACEMENT_3D('',#19794,#8676,#8677);
#7164=AXIS2_PLACEMENT_3D('',#19795,#8678,#8679);
#8538=DIRECTION('axis',(0.,0.,1.));
#8539=DIRECTION('refdir',(1.,0.,0.));
#8540=DIRECTION('center_axis',(0.,0.,1.));
#8541=DIRECTION('ref_axis',(1.,0.,0.));
#8542=DIRECTION('',(0.,0.,-1.));
#8543=DIRECTION('center_axis',(0.,0.,-1.));
#8544=DIRECTION('ref_axis',(1.,0.,0.));
#8545=DIRECTION('center_axis',(0.,0.,1.));
#8546=DIRECTION('ref_axis',(1.,0.,0.));
#8547=DIRECTION('',(0.,0.,-1.));
#8548=DIRECTION('center_axis',(0.,0.,1.));
#8549=DIRECTION('ref_axis',(1.,0.,0.));
#8550=DIRECTION('',(0.,0.,-1.));
#8551=DIRECTION('center_axis',(0.,0.,1.));
#8552=DIRECTION('ref_axis',(1.,0.,0.));
#8553=DIRECTION('',(0.,0.,-1.));
#8554=DIRECTION('center_axis',(0.,0.,1.));
#8555=DIRECTION('ref_axis',(1.,0.,0.));
#8556=DIRECTION('',(0.,0.,-1.));
#8557=DIRECTION('center_axis',(0.,0.,1.));
#8558=DIRECTION('ref_axis',(1.,0.,0.));
#8559=DIRECTION('',(0.,0.,-1.));
#8560=DIRECTION('center_axis',(0.,0.,1.));
#8561=DIRECTION('ref_axis',(1.,0.,0.));
#8562=DIRECTION('',(0.,0.,-1.));
#8563=DIRECTION('center_axis',(0.,0.,1.));
#8564=DIRECTION('ref_axis',(1.,0.,0.));
#8565=DIRECTION('',(0.,0.,-1.));
#8566=DIRECTION('center_axis',(0.,0.,1.));
#8567=DIRECTION('ref_axis',(1.,0.,0.));
#8568=DIRECTION('',(0.,0.,-1.));
#8569=DIRECTION('center_axis',(0.,0.,1.));
#8570=DIRECTION('ref_axis',(1.,0.,0.));
#8571=DIRECTION('',(0.,0.,-1.));
#8572=DIRECTION('center_axis',(0.,0.,1.));
#8573=DIRECTION('ref_axis',(1.,0.,0.));
#8574=DIRECTION('',(0.,0.,-1.));
#8575=DIRECTION('center_axis',(0.,0.,1.));
#8576=DIRECTION('ref_axis',(1.,0.,0.));
#8577=DIRECTION('',(0.,0.,-1.));
#8578=DIRECTION('center_axis',(0.,0.,1.));
#8579=DIRECTION('ref_axis',(1.,0.,0.));
#8580=DIRECTION('',(0.,0.,-1.));
#8581=DIRECTION('center_axis',(0.,0.,1.));
#8582=DIRECTION('ref_axis',(1.,9.40280585438808E-14,0.));
#8583=DIRECTION('',(0.,0.,1.));
#8584=DIRECTION('center_axis',(0.,0.,-1.));
#8585=DIRECTION('ref_axis',(1.,9.40280585438808E-14,0.));
#8586=DIRECTION('center_axis',(0.,0.,1.));
#8587=DIRECTION('ref_axis',(1.,9.40280585438808E-14,0.));
#8588=DIRECTION('',(0.,0.,1.));
#8589=DIRECTION('center_axis',(0.,0.,1.));
#8590=DIRECTION('ref_axis',(1.,9.40280585438808E-14,0.));
#8591=DIRECTION('',(0.,0.,1.));
#8592=DIRECTION('center_axis',(0.,0.,1.));
#8593=DIRECTION('ref_axis',(1.,9.40280585438808E-14,0.));
#8594=DIRECTION('',(0.,0.,1.));
#8595=DIRECTION('center_axis',(0.,0.,1.));
#8596=DIRECTION('ref_axis',(1.,9.40280585438808E-14,0.));
#8597=DIRECTION('',(0.,0.,1.));
#8598=DIRECTION('center_axis',(0.,0.,1.));
#8599=DIRECTION('ref_axis',(1.,9.40280585438808E-14,0.));
#8600=DIRECTION('',(0.,0.,1.));
#8601=DIRECTION('center_axis',(0.,0.,1.));
#8602=DIRECTION('ref_axis',(1.,9.40280585438808E-14,0.));
#8603=DIRECTION('',(0.,0.,1.));
#8604=DIRECTION('center_axis',(0.,0.,1.));
#8605=DIRECTION('ref_axis',(1.,9.40280585438808E-14,0.));
#8606=DIRECTION('',(0.,0.,1.));
#8607=DIRECTION('center_axis',(0.,0.,1.));
#8608=DIRECTION('ref_axis',(1.,9.40280585438808E-14,0.));
#8609=DIRECTION('',(0.,0.,1.));
#8610=DIRECTION('center_axis',(0.,0.,1.));
#8611=DIRECTION('ref_axis',(1.,9.40280585438808E-14,0.));
#8612=DIRECTION('',(0.,0.,1.));
#8613=DIRECTION('center_axis',(0.,0.,1.));
#8614=DIRECTION('ref_axis',(1.,9.40280585438808E-14,0.));
#8615=DIRECTION('',(0.,0.,1.));
#8616=DIRECTION('center_axis',(0.,0.,1.));
#8617=DIRECTION('ref_axis',(1.,9.40280585438808E-14,0.));
#8618=DIRECTION('',(0.,0.,1.));
#8619=DIRECTION('center_axis',(0.,0.,1.));
#8620=DIRECTION('ref_axis',(1.,9.40280585438808E-14,0.));
#8621=DIRECTION('',(0.,0.,1.));
#8622=DIRECTION('center_axis',(0.,0.,-1.));
#8623=DIRECTION('ref_axis',(1.,0.,0.));
#8624=DIRECTION('center_axis',(0.,0.,-1.));
#8625=DIRECTION('ref_axis',(1.,0.,0.));
#8626=DIRECTION('',(0.707106781186548,8.65956056235494E-17,0.707106781186547));
#8627=DIRECTION('center_axis',(0.,0.,1.));
#8628=DIRECTION('ref_axis',(1.,0.,0.));
#8629=DIRECTION('center_axis',(0.,0.,1.));
#8630=DIRECTION('ref_axis',(1.,9.40280585438808E-14,0.));
#8631=DIRECTION('center_axis',(0.,0.,-1.));
#8632=DIRECTION('ref_axis',(1.,9.40280585438808E-14,0.));
#8633=DIRECTION('center_axis',(0.,0.,1.));
#8634=DIRECTION('ref_axis',(1.,0.,0.));
#8635=DIRECTION('center_axis',(-1.60246890531964E-16,-1.,0.));
#8636=DIRECTION('ref_axis',(1.,-1.60246890531964E-16,0.));
#8637=DIRECTION('',(1.,-1.60246890531964E-16,0.));
#8638=DIRECTION('',(0.,0.,1.));
#8639=DIRECTION('',(1.,-1.60246890531964E-16,0.));
#8640=DIRECTION('',(0.,0.,1.));
#8641=DIRECTION('center_axis',(-0.866025403784439,-0.5,0.));
#8642=DIRECTION('ref_axis',(0.5,-0.866025403784439,0.));
#8643=DIRECTION('',(0.5,-0.866025403784439,0.));
#8644=DIRECTION('',(0.,0.,1.));
#8645=DIRECTION('',(0.5,-0.866025403784439,0.));
#8646=DIRECTION('center_axis',(-0.866025403784439,0.5,0.));
#8647=DIRECTION('ref_axis',(-0.5,-0.866025403784439,0.));
#8648=DIRECTION('',(-0.5,-0.866025403784439,0.));
#8649=DIRECTION('',(0.,0.,1.));
#8650=DIRECTION('',(-0.5,-0.866025403784439,0.));
#8651=DIRECTION('center_axis',(1.60246890531964E-16,1.,0.));
#8652=DIRECTION('ref_axis',(-1.,1.60246890531964E-16,0.));
#8653=DIRECTION('',(-1.,1.60246890531964E-16,0.));
#8654=DIRECTION('',(0.,0.,1.));
#8655=DIRECTION('',(-1.,1.60246890531964E-16,0.));
#8656=DIRECTION('center_axis',(0.866025403784439,0.5,0.));
#8657=DIRECTION('ref_axis',(-0.5,0.866025403784439,0.));
#8658=DIRECTION('',(-0.5,0.866025403784439,0.));
#8659=DIRECTION('',(0.,0.,1.));
#8660=DIRECTION('',(-0.5,0.866025403784439,0.));
#8661=DIRECTION('center_axis',(0.866025403784439,-0.5,0.));
#8662=DIRECTION('ref_axis',(0.5,0.866025403784439,0.));
#8663=DIRECTION('',(0.5,0.866025403784439,0.));
#8664=DIRECTION('',(0.5,0.866025403784439,0.));
#8665=DIRECTION('center_axis',(0.,0.,1.));
#8666=DIRECTION('ref_axis',(1.,0.,0.));
#8667=DIRECTION('center_axis',(0.,0.,1.));
#8668=DIRECTION('ref_axis',(1.,0.,0.));
#8669=DIRECTION('center_axis',(0.,0.,1.));
#8670=DIRECTION('ref_axis',(1.,0.,0.));
#8671=DIRECTION('center_axis',(0.,0.,1.));
#8672=DIRECTION('ref_axis',(1.,0.,0.));
#8673=DIRECTION('',(0.,0.,-1.));
#8674=DIRECTION('center_axis',(0.,0.,1.));
#8675=DIRECTION('ref_axis',(1.,0.,0.));
#8676=DIRECTION('center_axis',(0.,0.,1.));
#8677=DIRECTION('ref_axis',(1.,0.,0.));
#8678=DIRECTION('center_axis',(0.,0.,1.));
#8679=DIRECTION('ref_axis',(1.,0.,0.));
#17587=CARTESIAN_POINT('',(0.,0.,0.));
#17588=CARTESIAN_POINT('Origin',(0.,0.,0.));
#17589=CARTESIAN_POINT('',(-1.95633575083409,0.00127285042835199,0.22586969212423));
#17590=CARTESIAN_POINT('',(-1.95588099269616,0.00206992261158074,0.124130307875763));
#17591=CARTESIAN_POINT('',(-1.954,-2.39295984553393E-16,0.));
#17592=CARTESIAN_POINT('',(0.861525859670522,1.75382131162755,0.));
#17593=CARTESIAN_POINT('Ctrl Pts',(-1.95633575083409,0.00127285042835199,
0.22586969212423));
#17594=CARTESIAN_POINT('Ctrl Pts',(-1.95680045835965,0.0682528464970811,
0.222037453599974));
#17595=CARTESIAN_POINT('Ctrl Pts',(-1.95365942703396,0.135185904981779,
0.218205215075717));
#17596=CARTESIAN_POINT('Ctrl Pts',(-1.94676900820417,0.201727159714737,
0.214372976551461));
#17597=CARTESIAN_POINT('Ctrl Pts',(-1.88017550235509,0.84482528563818,0.1773357216495));
#17598=CARTESIAN_POINT('Ctrl Pts',(-1.46336852822225,1.45132678060953,0.14029846674754));
#17599=CARTESIAN_POINT('Ctrl Pts',(-0.886890238653646,1.74452948919289,
0.103261211845579));
#17600=CARTESIAN_POINT('Ctrl Pts',(-0.351142769057663,2.01701608937305,
0.0688408078970528));
#17601=CARTESIAN_POINT('Ctrl Pts',(0.322510092743222,2.01891187055583,0.0344204039485265));
#17602=CARTESIAN_POINT('Ctrl Pts',(0.86356802035368,1.756414520678,3.12250225675825E-16));
#17603=CARTESIAN_POINT('',(-0.861525859670558,1.75382131162753,0.));
#17604=CARTESIAN_POINT('Origin',(0.,0.,0.));
#17605=CARTESIAN_POINT('Ctrl Pts',(-0.861525859670558,1.75382131162753,
1.42247325030098E-15));
#17606=CARTESIAN_POINT('Ctrl Pts',(-1.44504958508736,1.46717821073411,0.0370673336485529));
#17607=CARTESIAN_POINT('Ctrl Pts',(-1.86921464413225,0.868908493151144,
0.0741346672971042));
#17608=CARTESIAN_POINT('Ctrl Pts',(-1.94383305148301,0.227162278519285,
0.111202000945656));
#17609=CARTESIAN_POINT('Ctrl Pts',(-1.95250816222439,0.152553081171747,
0.115511436589025));
#17610=CARTESIAN_POINT('Ctrl Pts',(-1.95645869249163,0.0773562420658186,
0.119820872232394));
#17611=CARTESIAN_POINT('Ctrl Pts',(-1.95588099269616,0.00206992261158074,
0.124130307875763));
#17612=CARTESIAN_POINT('Origin',(0.,0.,0.));
#17613=CARTESIAN_POINT('',(-1.95128228942929,0.000979822369055472,0.92586969212423));
#17614=CARTESIAN_POINT('',(-1.95119461725619,0.00092642636832007,0.824130307875761));
#17615=CARTESIAN_POINT('',(-1.954,-2.39295984553393E-16,0.));
#17616=CARTESIAN_POINT('Ctrl Pts',(-1.95128228942929,0.000979822369055472,
0.92586969212423));
#17617=CARTESIAN_POINT('Ctrl Pts',(-1.9524734062589,0.263895099571634,0.910927649678405));
#17618=CARTESIAN_POINT('Ctrl Pts',(-1.90305436999396,0.526380727998823,
0.89598560723258));
#17619=CARTESIAN_POINT('Ctrl Pts',(-1.80089851330331,0.766421656018886,
0.881043564786755));
#17620=CARTESIAN_POINT('Ctrl Pts',(-1.54768195889331,1.36141775981235,0.844006309884795));
#17621=CARTESIAN_POINT('Ctrl Pts',(-0.97044557322541,1.81851157863974,0.806969054982833));
#17622=CARTESIAN_POINT('Ctrl Pts',(-0.333248418269387,1.92861710553695,
0.769931800080872));
#17623=CARTESIAN_POINT('Ctrl Pts',(0.303948736686636,2.03872263243416,0.732894545178912));
#17624=CARTESIAN_POINT('Ctrl Pts',(1.00110666093079,1.80183986740118,0.695857290276951));
#17625=CARTESIAN_POINT('Ctrl Pts',(1.43929923459321,1.3263033286824,0.658820035374991));
#17626=CARTESIAN_POINT('Ctrl Pts',(1.87749180825564,0.850766789963622,0.62178278047303));
#17627=CARTESIAN_POINT('Ctrl Pts',(2.05671903133634,0.136576477559035,0.584745525571069));
#17628=CARTESIAN_POINT('Ctrl Pts',(1.89500173497496,-0.48949878222732,0.547708270669108));
#17629=CARTESIAN_POINT('Ctrl Pts',(1.73328443861357,-1.11557404201368,0.510671015767147));
#17630=CARTESIAN_POINT('Ctrl Pts',(1.23062262281009,-1.65353424918181,0.473633760865186));
#17631=CARTESIAN_POINT('Ctrl Pts',(0.616944482209929,-1.85739202336751,
0.436596505963226));
#17632=CARTESIAN_POINT('Ctrl Pts',(0.00326634160977092,-2.06124979755321,
0.399559251061265));
#17633=CARTESIAN_POINT('Ctrl Pts',(-0.721428123787067,-1.93100513875649,
0.362521996159304));
#17634=CARTESIAN_POINT('Ctrl Pts',(-1.22558533770282,-1.52603543092037,
0.325484741257344));
#17635=CARTESIAN_POINT('Ctrl Pts',(-1.67757748964075,-1.16296787052023,
0.292279724879639));
#17636=CARTESIAN_POINT('Ctrl Pts',(-1.95230922145719,-0.579085562119143,
0.259074708501934));
#17637=CARTESIAN_POINT('Ctrl Pts',(-1.95633575083409,0.00127285042835199,
0.22586969212423));
#17638=CARTESIAN_POINT('Ctrl Pts',(-1.95588099269616,0.00206992261158074,
0.124130307875763));
#17639=CARTESIAN_POINT('Ctrl Pts',(-1.95148964483908,-0.570214194837128,
0.156888205880946));
#17640=CARTESIAN_POINT('Ctrl Pts',(-1.68544890035158,-1.14766865010464,
0.189646103886129));
#17641=CARTESIAN_POINT('Ctrl Pts',(-1.24400073481116,-1.51148858380038,
0.222404001891312));
#17642=CARTESIAN_POINT('Ctrl Pts',(-0.744478255131947,-1.9231705198074,
0.259471335539864));
#17643=CARTESIAN_POINT('Ctrl Pts',(-0.0203615401169106,-2.06131168014067,
0.296538669188416));
#17644=CARTESIAN_POINT('Ctrl Pts',(0.596117854997422,-1.86404025704795,
0.333606002836968));
#17645=CARTESIAN_POINT('Ctrl Pts',(1.21259725011176,-1.66676883395523,0.37067333648552));
#17646=CARTESIAN_POINT('Ctrl Pts',(1.72143932532539,-1.13408482743652,0.407740670134072));
#17647=CARTESIAN_POINT('Ctrl Pts',(1.88977433415544,-0.509313521695289,
0.444808003782624));
#17648=CARTESIAN_POINT('Ctrl Pts',(2.05810934298549,0.115457784045944,0.481875337431176));
#17649=CARTESIAN_POINT('Ctrl Pts',(1.88593728543196,0.832316389009701,0.518942671079728));
#17650=CARTESIAN_POINT('Ctrl Pts',(1.45200572115437,1.31246709551687,0.55601000472828));
#17651=CARTESIAN_POINT('Ctrl Pts',(1.01807415687679,1.79261780202404,0.593077338376832));
#17652=CARTESIAN_POINT('Ctrl Pts',(0.322383085875136,2.03606061007462,0.630144672025384));
#17653=CARTESIAN_POINT('Ctrl Pts',(-0.316275274467243,1.93146093707914,
0.667212005673936));
#17654=CARTESIAN_POINT('Ctrl Pts',(-0.954933634809622,1.82686126408366,
0.704279339322488));
#17655=CARTESIAN_POINT('Ctrl Pts',(-1.53655928449273,1.37421911004211,0.741346672971039));
#17656=CARTESIAN_POINT('Ctrl Pts',(-1.79472283882274,0.780804664464737,
0.778414006619591));
#17657=CARTESIAN_POINT('Ctrl Pts',(-1.9008565659387,0.53684580281587,0.793652773704981));
#17658=CARTESIAN_POINT('Ctrl Pts',(-1.95232138952433,0.269094766021062,
0.808891540790371));
#17659=CARTESIAN_POINT('Ctrl Pts',(-1.95119461725619,0.00092642636832007,
0.824130307875761));
#17660=CARTESIAN_POINT('Origin',(0.,0.,0.));
#17661=CARTESIAN_POINT('',(-1.95279539392324,-0.00168116113097749,1.62586969212423));
#17662=CARTESIAN_POINT('',(-1.95283689833027,-0.00169757742976787,1.52413030787576));
#17663=CARTESIAN_POINT('',(-1.954,-2.39295984553393E-16,0.));
#17664=CARTESIAN_POINT('Ctrl Pts',(-1.95279539392324,-0.00168116113097749,
1.62586969212423));
#17665=CARTESIAN_POINT('Ctrl Pts',(-1.94903666796486,0.455824327828861,
1.59981784575684));
#17666=CARTESIAN_POINT('Ctrl Pts',(-1.78857561082415,0.915704606010159,
1.57376599938944));
#17667=CARTESIAN_POINT('Ctrl Pts',(-1.49502845554474,1.26314111490869,1.54771415302205));
#17668=CARTESIAN_POINT('Ctrl Pts',(-1.07769984618227,1.75708286325356,1.51067689812009));
#17669=CARTESIAN_POINT('Ctrl Pts',(-0.391383019514876,2.02375783115006,
1.47363964321813));
#17670=CARTESIAN_POINT('Ctrl Pts',(0.249960502791804,1.9411735695446,1.43660238831617));
#17671=CARTESIAN_POINT('Ctrl Pts',(0.891304025098484,1.85858930793915,1.39956513341421));
#17672=CARTESIAN_POINT('Ctrl Pts',(1.48767424304445,1.42674581683174,1.36252787851224));
#17673=CARTESIAN_POINT('Ctrl Pts',(1.76625632450792,0.843193022913364,1.32549062361028));
#17674=CARTESIAN_POINT('Ctrl Pts',(2.04483840597138,0.259640228994984,1.28845336870832));
#17675=CARTESIAN_POINT('Ctrl Pts',(2.00563235095235,-0.475621867734372,
1.25141611380636));
#17676=CARTESIAN_POINT('Ctrl Pts',(1.66657351619212,-1.026240070129,1.2143788589044));
#17677=CARTESIAN_POINT('Ctrl Pts',(1.32751468143189,-1.57685827252363,1.17734160400244));
#17678=CARTESIAN_POINT('Ctrl Pts',(0.688603066930477,-1.94283258058353,
1.14030434910048));
#17679=CARTESIAN_POINT('Ctrl Pts',(0.0421139319386674,-1.95674712405518,
1.10326709419852));
#17680=CARTESIAN_POINT('Ctrl Pts',(-0.604375203053146,-1.97066166752684,
1.06622983929656));
#17681=CARTESIAN_POINT('Ctrl Pts',(-1.25844185853535,-1.63251644641023,
1.0291925843946));
#17682=CARTESIAN_POINT('Ctrl Pts',(-1.62087682470039,-1.09699464147216,
0.992155329492637));
#17683=CARTESIAN_POINT('Ctrl Pts',(-1.83709364746835,-0.777519883250448,
0.970060117036501));
#17684=CARTESIAN_POINT('Ctrl Pts',(-1.94952095194778,-0.387800287767629,
0.947964904580365));
#17685=CARTESIAN_POINT('Ctrl Pts',(-1.95128228942929,0.000979822369055472,
0.92586969212423));
#17686=CARTESIAN_POINT('Ctrl Pts',(-1.95119461725619,0.00092642636832007,
0.824130307875761));
#17687=CARTESIAN_POINT('Ctrl Pts',(-1.94958058750438,-0.38320769809472,
0.845958874438923));
#17688=CARTESIAN_POINT('Ctrl Pts',(-1.84005520872064,-0.768198075607766,
0.867787441002085));
#17689=CARTESIAN_POINT('Ctrl Pts',(-1.62872406172904,-1.08534175300753,
0.889616007565247));
#17690=CARTESIAN_POINT('Ctrl Pts',(-1.26986027132842,-1.62388698778921,
0.926683341213799));
#17691=CARTESIAN_POINT('Ctrl Pts',(-0.617431231550254,-1.96679072023937,
0.963750674862351));
#17692=CARTESIAN_POINT('Ctrl Pts',(0.0296497544693555,-1.9569836764894,
1.0008180085109));
#17693=CARTESIAN_POINT('Ctrl Pts',(0.676730740488965,-1.94717663273943,
1.03788534215945));
#17694=CARTESIAN_POINT('Ctrl Pts',(1.31846367275002,-1.58465881278932,1.07495267580801));
#17695=CARTESIAN_POINT('Ctrl Pts',(1.66085075139256,-1.03549895096933,1.11202000945656));
#17696=CARTESIAN_POINT('Ctrl Pts',(2.00323783003509,-0.486339089149333,
1.14908734310511));
#17697=CARTESIAN_POINT('Ctrl Pts',(2.04627905505911,0.249462814540552,1.18615467675366));
#17698=CARTESIAN_POINT('Ctrl Pts',(1.77025280539679,0.834799217616478,1.22322201040222));
#17699=CARTESIAN_POINT('Ctrl Pts',(1.49422655573448,1.4201356206924,1.26028934405077));
#17700=CARTESIAN_POINT('Ctrl Pts',(0.899132831385847,1.85500652315437,1.29735667769932));
#17701=CARTESIAN_POINT('Ctrl Pts',(0.257608856151057,1.94018461251091,1.33442401134787));
#17702=CARTESIAN_POINT('Ctrl Pts',(-0.383915119083735,2.02536270186746,
1.37149134499642));
#17703=CARTESIAN_POINT('Ctrl Pts',(-1.07186934520468,1.76084797811858,1.40855867864497));
#17704=CARTESIAN_POINT('Ctrl Pts',(-1.49107575958572,1.26782285617356,1.44562601229353));
#17705=CARTESIAN_POINT('Ctrl Pts',(-1.78701921370236,0.919766260307501,
1.47179411082094));
#17706=CARTESIAN_POINT('Ctrl Pts',(-1.94902381498454,0.457824381443284,
1.49796220934835));
#17707=CARTESIAN_POINT('Ctrl Pts',(-1.95283689833027,-0.00169757742976787,
1.52413030787576));
#17708=CARTESIAN_POINT('Origin',(0.,0.,0.));
#17709=CARTESIAN_POINT('',(-1.95719985818546,4.05420783899653E-5,2.32586969212423));
#17710=CARTESIAN_POINT('',(-1.95721255371923,9.84009623044488E-6,2.22413030787576));
#17711=CARTESIAN_POINT('',(-1.954,-2.39295984553393E-16,0.));
#17712=CARTESIAN_POINT('Ctrl Pts',(-1.95719985818546,4.05420783900091E-5,
2.32586969212423));
#17713=CARTESIAN_POINT('Ctrl Pts',(-1.95720052181173,0.00221238218774959,
2.32574529673723));
#17714=CARTESIAN_POINT('Ctrl Pts',(-1.95719721915126,0.00438422021875816,
2.32562090135023));
#17715=CARTESIAN_POINT('Ctrl Pts',(-1.95718994413828,0.00655604494350104,
2.32549650596323));
#17716=CARTESIAN_POINT('Ctrl Pts',(-1.95502389508506,0.653191164393938,
2.28845925106126));
#17717=CARTESIAN_POINT('Ctrl Pts',(-1.6007166691436,1.2986467097638,2.2514219961593));
#17718=CARTESIAN_POINT('Ctrl Pts',(-1.05634917726868,1.64765344582725,2.21438474125734));
#17719=CARTESIAN_POINT('Ctrl Pts',(-0.511981685393759,1.9966601818907,2.17734748635538));
#17720=CARTESIAN_POINT('Ctrl Pts',(0.222446072414618,2.04921810864774,2.14031023145342));
#17721=CARTESIAN_POINT('Ctrl Pts',(0.810963756254723,1.78128415395532,2.10327297655146));
#17722=CARTESIAN_POINT('Ctrl Pts',(1.39948144009482,1.51335019926291,2.0662357216495));
#17723=CARTESIAN_POINT('Ctrl Pts',(1.84208904996665,0.924924363121033,2.02919846674754));
#17724=CARTESIAN_POINT('Ctrl Pts',(1.93631189757409,0.285187129558038,1.99216121184558));
#17725=CARTESIAN_POINT('Ctrl Pts',(2.03053474518152,-0.354550104004963,
1.95512395694362));
#17726=CARTESIAN_POINT('Ctrl Pts',(1.77637283052455,-1.04559873498909,1.91808670204166));
#17727=CARTESIAN_POINT('Ctrl Pts',(1.29009472793977,-1.47183255494777,1.8810494471397));
#17728=CARTESIAN_POINT('Ctrl Pts',(0.803816625355003,-1.89806637490645,
1.84401219223774));
#17729=CARTESIAN_POINT('Ctrl Pts',(0.0854223348424371,-2.05948538383969,
1.80697493733577));
#17730=CARTESIAN_POINT('Ctrl Pts',(-0.536452459305869,-1.88224710468127,
1.76993768243381));
#17731=CARTESIAN_POINT('Ctrl Pts',(-1.15832725345417,-1.70500882552285,
1.73290042753185));
#17732=CARTESIAN_POINT('Ctrl Pts',(-1.68368255123822,-1.18911325827277,
1.69586317262989));
#17733=CARTESIAN_POINT('Ctrl Pts',(-1.87219000410148,-0.570561210251106,
1.65882591772793));
#17734=CARTESIAN_POINT('Ctrl Pts',(-1.92810212250753,-0.387096021877988,
1.64784050919336));
#17735=CARTESIAN_POINT('Ctrl Pts',(-1.95438035414602,-0.194599721764027,
1.6368551006588));
#17736=CARTESIAN_POINT('Ctrl Pts',(-1.95279539392324,-0.00168116113097727,
1.62586969212423));
#17737=CARTESIAN_POINT('Ctrl Pts',(-1.95283689833027,-0.00169757742976787,
1.52413030787576));
#17738=CARTESIAN_POINT('Ctrl Pts',(-1.95442507990479,-0.193092373189868,
1.5350295429969));
#17739=CARTESIAN_POINT('Ctrl Pts',(-1.92857030457963,-0.38406736287639,
1.54592877811804));
#17740=CARTESIAN_POINT('Ctrl Pts',(-1.87352018127017,-0.566218843228074,
1.55682801323918));
#17741=CARTESIAN_POINT('Ctrl Pts',(-1.68629958593245,-1.18569990054353,
1.59389534688773));
#17742=CARTESIAN_POINT('Ctrl Pts',(-1.16139979261586,-1.70312649503327,
1.63096268053629));
#17743=CARTESIAN_POINT('Ctrl Pts',(-0.539298197806726,-1.88144579938109,
1.66803001418484));
#17744=CARTESIAN_POINT('Ctrl Pts',(0.0828033970024101,-2.0597651037289,
1.70509734783339));
#17745=CARTESIAN_POINT('Ctrl Pts',(0.802106793304097,-1.89897711793479,
1.74216468148194));
#17746=CARTESIAN_POINT('Ctrl Pts',(1.28907099594446,-1.47274481385923,1.77923201513049));
#17747=CARTESIAN_POINT('Ctrl Pts',(1.77603519858483,-1.04651250978366,1.81629934877905));
#17748=CARTESIAN_POINT('Ctrl Pts',(2.03066020756387,-0.35483588742664,1.8533666824276));
#17749=CARTESIAN_POINT('Ctrl Pts',(1.9362922595033,0.285400693385207,1.89043401607615));
#17750=CARTESIAN_POINT('Ctrl Pts',(1.84192431144273,0.925637274197054,1.9275013497247));
#17751=CARTESIAN_POINT('Ctrl Pts',(1.39856340634255,1.51443381346373,1.96456868337325));
#17752=CARTESIAN_POINT('Ctrl Pts',(0.809330598539892,1.78203960359444,2.00163601702181));
#17753=CARTESIAN_POINT('Ctrl Pts',(0.220097790737234,2.04964539372514,2.03870335067036));
#17754=CARTESIAN_POINT('Ctrl Pts',(-0.515006919767895,1.99606043471988,
2.07577068431891));
#17755=CARTESIAN_POINT('Ctrl Pts',(-1.05920324210055,1.6458340532769,2.11283801796746));
#17756=CARTESIAN_POINT('Ctrl Pts',(-1.60384141728657,1.29532331025408,2.1499354479369));
#17757=CARTESIAN_POINT('Ctrl Pts',(-1.95726085438506,0.64768924107042,2.18703287790633));
#17758=CARTESIAN_POINT('Ctrl Pts',(-1.95721255371923,9.84009623044488E-6,
2.22413030787576));
#17759=CARTESIAN_POINT('Origin',(0.,0.,0.));
#17760=CARTESIAN_POINT('',(-1.95267758926504,0.00165506900100115,3.02586969212423));
#17761=CARTESIAN_POINT('',(-1.95280791655641,0.00169181170498602,2.92413030787576));
#17762=CARTESIAN_POINT('',(-1.954,-2.39295984553393E-16,0.));
#17763=CARTESIAN_POINT('Ctrl Pts',(-1.95267758926504,0.00165506900100115,
3.02586969212423));
#17764=CARTESIAN_POINT('Ctrl Pts',(-1.95426628302477,0.198972830964143,
3.01463549281566));
#17765=CARTESIAN_POINT('Ctrl Pts',(-1.92675962108266,0.395857959120396,
3.00340129350709));
#17766=CARTESIAN_POINT('Ctrl Pts',(-1.86832558386105,0.583090877542938,
2.99216709419852));
#17767=CARTESIAN_POINT('Ctrl Pts',(-1.67567844701734,1.20036613990759,2.95512983929656));
#17768=CARTESIAN_POINT('Ctrl Pts',(-1.14687877096073,1.7127306304502,2.9180925843946));
#17769=CARTESIAN_POINT('Ctrl Pts',(-0.52383054918719,1.88579877362532,2.88105532949264));
#17770=CARTESIAN_POINT('Ctrl Pts',(0.0992176725863465,2.05886691680043,
2.84401807459068));
#17771=CARTESIAN_POINT('Ctrl Pts',(0.81651444007682,1.89263871260806,2.80698081968871));
#17772=CARTESIAN_POINT('Ctrl Pts',(1.29992613215786,1.46315669344762,2.76994356478675));
#17773=CARTESIAN_POINT('Ctrl Pts',(1.7833378242389,1.03367467428718,2.73290630988479));
#17774=CARTESIAN_POINT('Ctrl Pts',(2.03286444091049,0.340938840158676,2.69586905498283));
#17775=CARTESIAN_POINT('Ctrl Pts',(1.93435786935885,-0.298152799828459,
2.65883180008087));
#17776=CARTESIAN_POINT('Ctrl Pts',(1.8358512978072,-0.937244439815588,2.62179454517891));
#17777=CARTESIAN_POINT('Ctrl Pts',(1.38931153803231,-1.52269188566136,2.58475729027695));
#17778=CARTESIAN_POINT('Ctrl Pts',(0.799012072181727,-1.78667713026121,
2.54772003537499));
#17779=CARTESIAN_POINT('Ctrl Pts',(0.208712606331136,-2.05066237486107,
2.51068278047303));
#17780=CARTESIAN_POINT('Ctrl Pts',(-0.525346565595159,-1.99318541821502,
2.47364552557107));
#17781=CARTESIAN_POINT('Ctrl Pts',(-1.06736371547582,-1.64053959312649,
2.43660827066911));
#17782=CARTESIAN_POINT('Ctrl Pts',(-1.60756041637074,-1.28907818394574,
2.39969541115415));
#17783=CARTESIAN_POINT('Ctrl Pts',(-1.95700293493792,-0.644427317850318,
2.36278255163919));
#17784=CARTESIAN_POINT('Ctrl Pts',(-1.95719985818546,4.05420783899653E-5,
2.32586969212423));
#17785=CARTESIAN_POINT('Ctrl Pts',(-1.95721255371923,9.84009623044488E-6,
2.22413030787576));
#17786=CARTESIAN_POINT('Ctrl Pts',(-1.95716433142391,-0.646618665056022,
2.26116754520343));
#17787=CARTESIAN_POINT('Ctrl Pts',(-1.60505607381363,-1.29329214304674,
2.2982047825311));
#17788=CARTESIAN_POINT('Ctrl Pts',(-1.0618695239415,-1.64411505913035,2.33524201985877));
#17789=CARTESIAN_POINT('Ctrl Pts',(-0.518241582705361,-1.99522305260678,
2.37230935350733));
#17790=CARTESIAN_POINT('Ctrl Pts',(0.216775315978968,-2.04999947469641,
2.40937668715588));
#17791=CARTESIAN_POINT('Ctrl Pts',(0.806441097699488,-1.78334909096271,
2.44644402080443));
#17792=CARTESIAN_POINT('Ctrl Pts',(1.39610687942001,-1.516698707229,2.48351135445298));
#17793=CARTESIAN_POINT('Ctrl Pts',(1.84042154417672,-0.928621517671956,
2.52057868810153));
#17794=CARTESIAN_POINT('Ctrl Pts',(1.93582711194427,-0.288538757100728,
2.55764602175009));
#17795=CARTESIAN_POINT('Ctrl Pts',(2.03123267971181,0.351544003470497,2.59471335539864));
#17796=CARTESIAN_POINT('Ctrl Pts',(1.77772915049019,1.04363233505591,2.63178068904719));
#17797=CARTESIAN_POINT('Ctrl Pts',(1.29145643683783,1.470653423467,2.66884802269574));
#17798=CARTESIAN_POINT('Ctrl Pts',(0.805183723185476,1.89767451187809,2.7059153563443));
#17799=CARTESIAN_POINT('Ctrl Pts',(0.0861418251023859,2.05962835711487,
2.74298268999285));
#17800=CARTESIAN_POINT('Ctrl Pts',(-0.53624795552402,1.882317548121,2.7800500236414));
#17801=CARTESIAN_POINT('Ctrl Pts',(-1.15863773615042,1.70500673912713,2.81711735728995));
#17802=CARTESIAN_POINT('Ctrl Pts',(-1.68437539932014,1.18843127590261,2.8541846909385));
#17803=CARTESIAN_POINT('Ctrl Pts',(-1.87259989616401,0.569254644402596,
2.89125202458705));
#17804=CARTESIAN_POINT('Ctrl Pts',(-1.92825085816542,0.386187212853816,
2.90221145234996));
#17805=CARTESIAN_POINT('Ctrl Pts',(-1.95439762435419,0.194150753541291,
2.91317088011286));
#17806=CARTESIAN_POINT('Ctrl Pts',(-1.95280791655641,0.00169181170498602,
2.92413030787576));
#17807=CARTESIAN_POINT('Origin',(0.,0.,0.));
#17808=CARTESIAN_POINT('',(-1.95135083467133,-0.00103713828173369,3.72586969212423));
#17809=CARTESIAN_POINT('',(-1.95121488712599,-0.000926387452031019,3.62413030787576));
#17810=CARTESIAN_POINT('',(-1.954,-2.39295984553393E-16,0.));
#17811=CARTESIAN_POINT('Ctrl Pts',(-1.95135083467133,-0.00103713828173369,
3.72586969212423));
#17812=CARTESIAN_POINT('Ctrl Pts',(-1.94945690425454,0.392085240919391,
3.70352568889409));
#17813=CARTESIAN_POINT('Ctrl Pts',(-1.83430205983262,0.786228342622907,
3.68118168566395));
#17814=CARTESIAN_POINT('Ctrl Pts',(-1.61349106342003,1.10782762515327,3.65883768243382));
#17815=CARTESIAN_POINT('Ctrl Pts',(-1.24747638489286,1.64090822314112,3.62180042753185));
#17816=CARTESIAN_POINT('Ctrl Pts',(-0.591159457848277,1.9746664586804,3.58476317262989));
#17817=CARTESIAN_POINT('Ctrl Pts',(0.0552218529205667,1.95642173514589,
3.54772591772793));
#17818=CARTESIAN_POINT('Ctrl Pts',(0.70160316368942,1.93817701161139,3.51068866282597));
#17819=CARTESIAN_POINT('Ctrl Pts',(1.33804885818252,1.5679293290031,3.47365140792401));
#17820=CARTESIAN_POINT('Ctrl Pts',(1.67341133910821,1.01505169766431,3.43661415302205));
#17821=CARTESIAN_POINT('Ctrl Pts',(2.0087738200339,0.462174066325523,3.39957689812009));
#17822=CARTESIAN_POINT('Ctrl Pts',(2.04305308739216,-0.273333513743766,
3.36253964321813));
#17823=CARTESIAN_POINT('Ctrl Pts',(1.76056779332365,-0.855006727399908,
3.32550238831617));
#17824=CARTESIAN_POINT('Ctrl Pts',(1.47808249925514,-1.43667994105605,3.2884651334142));
#17825=CARTESIAN_POINT('Ctrl Pts',(0.878832643759864,-1.86451878829905,
3.25142787851224));
#17826=CARTESIAN_POINT('Ctrl Pts',(0.236950265307058,-1.94280468152938,
3.21439062361029));
#17827=CARTESIAN_POINT('Ctrl Pts',(-0.404932113145755,-2.02109057475972,
3.17735336870832));
#17828=CARTESIAN_POINT('Ctrl Pts',(-1.0894470145561,-1.74982351397736,3.14031611380636));
#17829=CARTESIAN_POINT('Ctrl Pts',(-1.50345716644585,-1.25309696649286,
3.1032788589044));
#17830=CARTESIAN_POINT('Ctrl Pts',(-1.7918890978543,-0.907038308706706,
3.07747580331101));
#17831=CARTESIAN_POINT('Ctrl Pts',(-1.94902862841993,-0.451550454744232,
3.05167274771762));
#17832=CARTESIAN_POINT('Ctrl Pts',(-1.95267758926504,0.00165506900100115,
3.02586969212423));
#17833=CARTESIAN_POINT('Ctrl Pts',(-1.95280791655641,0.00169181170498602,
2.92413030787576));
#17834=CARTESIAN_POINT('Ctrl Pts',(-1.94902086284632,-0.456790150037774,
2.95023821376141));
#17835=CARTESIAN_POINT('Ctrl Pts',(-1.78782842975758,-0.917669713651943,
2.97634611964706));
#17836=CARTESIAN_POINT('Ctrl Pts',(-1.49312888403822,-1.26540402906769,
3.00245402553271));
#17837=CARTESIAN_POINT('Ctrl Pts',(-1.07472204455054,-1.75910827126244,
3.03952135918126));
#17838=CARTESIAN_POINT('Ctrl Pts',(-0.387197035057166,-2.02473895587643,
3.07658869282981));
#17839=CARTESIAN_POINT('Ctrl Pts',(0.254463965370863,-1.94060024520244,
3.11365602647837));
#17840=CARTESIAN_POINT('Ctrl Pts',(0.896124965798891,-1.85646153452846,
3.15072336012692));
#17841=CARTESIAN_POINT('Ctrl Pts',(1.49192195716157,-1.42255342856649,3.18779069377547));
#17842=CARTESIAN_POINT('Ctrl Pts',(1.76889696399884,-0.837666253363929,
3.22485802742402));
#17843=CARTESIAN_POINT('Ctrl Pts',(2.04587197083611,-0.252779078161363,
3.26192536107257));
#17844=CARTESIAN_POINT('Ctrl Pts',(2.00402499314796,0.483087166281804,3.29899269472113));
#17845=CARTESIAN_POINT('Ctrl Pts',(1.66252777312397,1.03280328468034,3.33606002836968));
#17846=CARTESIAN_POINT('Ctrl Pts',(1.32103055309999,1.58251940307888,3.37312736201823));
#17847=CARTESIAN_POINT('Ctrl Pts',(0.679883090740172,1.94608539543278,3.41019469566678));
#17848=CARTESIAN_POINT('Ctrl Pts',(0.0328201913788997,1.95693741757976,
3.44726202931533));
#17849=CARTESIAN_POINT('Ctrl Pts',(-0.614242707982372,1.96778943972675,
3.48432936296388));
#17850=CARTESIAN_POINT('Ctrl Pts',(-1.2672210443451,1.62592749166683,3.52139669661244));
#17851=CARTESIAN_POINT('Ctrl Pts',(-1.62695982484692,1.08797194339114,3.55846403026099));
#17852=CARTESIAN_POINT('Ctrl Pts',(-1.83939041447971,0.770301954748211,
3.58035278946591));
#17853=CARTESIAN_POINT('Ctrl Pts',(-1.94956657085447,0.384252923937107,
3.60224154867084));
#17854=CARTESIAN_POINT('Ctrl Pts',(-1.95121488712599,-0.000926387452031019,
3.62413030787576));
#17855=CARTESIAN_POINT('Origin',(0.,0.,0.));
#17856=CARTESIAN_POINT('',(-1.95645531603829,-0.0010761721163155,4.42586969212423));
#17857=CARTESIAN_POINT('',(-1.95619906720822,-0.0012405029508829,4.32413030787576));
#17858=CARTESIAN_POINT('',(-1.954,-2.39295984553393E-16,0.));
#17859=CARTESIAN_POINT('Ctrl Pts',(-1.95645531603829,-0.0010761721163155,
4.42586969212423));
#17860=CARTESIAN_POINT('Ctrl Pts',(-1.95258058399789,0.583590658408003,
4.39241588497252));
#17861=CARTESIAN_POINT('Ctrl Pts',(-1.67315132747224,1.17147065165432,4.35896207782082));
#17862=CARTESIAN_POINT('Ctrl Pts',(-1.21532426049127,1.53415201354063,4.32550827066911));
#17863=CARTESIAN_POINT('Ctrl Pts',(-0.708456456061838,1.93568245781738,
4.28847101576715));
#17864=CARTESIAN_POINT('Ctrl Pts',(0.0170747010795776,2.06118547981998,
4.25143376086519));
#17865=CARTESIAN_POINT('Ctrl Pts',(0.629368696890541,1.85324863473949,4.21439650596323));
#17866=CARTESIAN_POINT('Ctrl Pts',(1.2416626927015,1.64531178965899,4.17735925106126));
#17867=CARTESIAN_POINT('Ctrl Pts',(1.740719527182,1.10393507749541,4.1403219961593));
#17868=CARTESIAN_POINT('Ctrl Pts',(1.89824132742874,0.476775965869676,4.10328474125734));
#17869=CARTESIAN_POINT('Ctrl Pts',(2.05576312767549,-0.15038314575607,4.06624748635538));
#17870=CARTESIAN_POINT('Ctrl Pts',(1.87174989368847,-0.863324656843973,
4.02921023145342));
#17871=CARTESIAN_POINT('Ctrl Pts',(1.43038007369796,-1.33590729601914,3.99217297655146));
#17872=CARTESIAN_POINT('Ctrl Pts',(0.989010253707457,-1.80848993519431,
3.9551357216495));
#17873=CARTESIAN_POINT('Ctrl Pts',(0.290283847713488,-2.04071370245675,
3.91809846674754));
#17874=CARTESIAN_POINT('Ctrl Pts',(-0.346160695897863,-1.92634582341936,
3.88106121184558));
#17875=CARTESIAN_POINT('Ctrl Pts',(-0.982605239509219,-1.81197794438196,
3.84402395694362));
#17876=CARTESIAN_POINT('Ctrl Pts',(-1.55676792073795,-1.35101841904471,
3.80698670204166));
#17877=CARTESIAN_POINT('Ctrl Pts',(-1.80599304634745,-0.754337176157871,
3.7699494471397));
#17878=CARTESIAN_POINT('Ctrl Pts',(-1.90486450707571,-0.517624501506378,
3.75525619546788));
#17879=CARTESIAN_POINT('Ctrl Pts',(-1.95259626934014,-0.259551514418081,
3.74056294379605));
#17880=CARTESIAN_POINT('Ctrl Pts',(-1.95135083467133,-0.00103713828173369,
3.72586969212423));
#17881=CARTESIAN_POINT('Ctrl Pts',(-1.95121488712599,-0.000926387452031019,
3.62413030787576));
#17882=CARTESIAN_POINT('Ctrl Pts',(-1.95235789806598,-0.268025714432167,
3.63930888231939));
#17883=CARTESIAN_POINT('Ctrl Pts',(-1.90131408798319,-0.534706827138703,
3.65448745676302));
#17884=CARTESIAN_POINT('Ctrl Pts',(-1.79599159513475,-0.777878789707524,
3.66966603120664));
#17885=CARTESIAN_POINT('Ctrl Pts',(-1.53878536027985,-1.37172482603906,
3.7067333648552));
#17886=CARTESIAN_POINT('Ctrl Pts',(-0.95787366592914,-1.82536775021069,
3.74380069850375));
#17887=CARTESIAN_POINT('Ctrl Pts',(-0.319394948990622,-1.93097594180636,
3.7808680321523));
#17888=CARTESIAN_POINT('Ctrl Pts',(0.319083767947896,-2.03658413340203,
3.81793536580085));
#17889=CARTESIAN_POINT('Ctrl Pts',(1.01512950747422,-1.79415759242175,3.85500269944941));
#17890=CARTESIAN_POINT('Ctrl Pts',(1.44985640976405,-1.31476142791748,3.89207003309796));
#17891=CARTESIAN_POINT('Ctrl Pts',(1.88458331205388,-0.835365263413203,
3.92913736674651));
#17892=CARTESIAN_POINT('Ctrl Pts',(2.05799137710721,-0.118999475384943,
3.96620470039506));
#17893=CARTESIAN_POINT('Ctrl Pts',(1.89063556735747,0.506140664950446,4.00327203404361));
#17894=CARTESIAN_POINT('Ctrl Pts',(1.72327975760774,1.13128080528583,4.04033936769217));
#17895=CARTESIAN_POINT('Ctrl Pts',(1.21516007305495,1.66519529792834,4.07740670134072));
#17896=CARTESIAN_POINT('Ctrl Pts',(0.599066075218673,1.86327696781671,4.11447403498927));
#17897=CARTESIAN_POINT('Ctrl Pts',(-0.0170279226176054,2.06135863770508,
4.15154136863782));
#17898=CARTESIAN_POINT('Ctrl Pts',(-0.74109623373737,1.92360748483931,4.18860870228637));
#17899=CARTESIAN_POINT('Ctrl Pts',(-1.24141475891726,1.51313271645821,4.22567603593493));
#17900=CARTESIAN_POINT('Ctrl Pts',(-1.68437887571559,1.14971304660178,4.25849412658187));
#17901=CARTESIAN_POINT('Ctrl Pts',(-1.95195229526599,0.572513574095349,
4.29131221722882));
#17902=CARTESIAN_POINT('Ctrl Pts',(-1.95619906720822,-0.0012405029508829,
4.32413030787576));
#17903=CARTESIAN_POINT('Origin',(0.,0.,0.));
#17904=CARTESIAN_POINT('',(-1.95458379985314,0.00173431571939442,5.12586969212423));
#17905=CARTESIAN_POINT('',(-1.95503514488101,0.00166188402949293,5.02413030787576));
#17906=CARTESIAN_POINT('',(-1.954,-2.39295984553393E-16,0.));
#17907=CARTESIAN_POINT('Ctrl Pts',(-1.95458379985314,0.00173431571939442,
5.12586969212423));
#17908=CARTESIAN_POINT('Ctrl Pts',(-1.95579765110671,0.133598995356774,
5.11834333595291));
#17909=CARTESIAN_POINT('Ctrl Pts',(-1.94359203725346,0.26524025398885,5.1108169797816));
#17910=CARTESIAN_POINT('Ctrl Pts',(-1.9171424819943,0.393954518342425,5.10329062361028));
#17911=CARTESIAN_POINT('Ctrl Pts',(-1.78698402312272,1.02735837405563,5.06625336870832));
#17912=CARTESIAN_POINT('Ctrl Pts',(-1.31188979988961,1.58988121587218,5.02921611380637));
#17913=CARTESIAN_POINT('Ctrl Pts',(-0.709195781064526,1.82419209594539,
4.9921788589044));
#17914=CARTESIAN_POINT('Ctrl Pts',(-0.10650176223944,2.0585029760186,4.95514160400244));
#17915=CARTESIAN_POINT('Ctrl Pts',(0.623792052177624,1.96460189434848,4.91810434910048));
#17916=CARTESIAN_POINT('Ctrl Pts',(1.14760642930858,1.58544471433065,4.88106709419852));
#17917=CARTESIAN_POINT('Ctrl Pts',(1.67142080643954,1.20628753431283,4.84402983929656));
#17918=CARTESIAN_POINT('Ctrl Pts',(1.98875574628439,0.541874255947292,4.8069925843946));
#17919=CARTESIAN_POINT('Ctrl Pts',(1.95444363113096,-0.103853509912194,
4.76995532949264));
#17920=CARTESIAN_POINT('Ctrl Pts',(1.92013151597754,-0.749581275771674,
4.73291807459068));
#17921=CARTESIAN_POINT('Ctrl Pts',(1.53417234582584,-1.3766235291251,4.69588081968872));
#17922=CARTESIAN_POINT('Ctrl Pts',(0.973126487121711,-1.69813435830372,
4.65884356478676));
#17923=CARTESIAN_POINT('Ctrl Pts',(0.412080628417575,-2.01964518748234,
4.62180630988479));
#17924=CARTESIAN_POINT('Ctrl Pts',(-0.324051918839002,-2.03562459248615,
4.58476905498283));
#17925=CARTESIAN_POINT('Ctrl Pts',(-0.898520942843956,-1.73876265604603,
4.54773180008087));
#17926=CARTESIAN_POINT('Ctrl Pts',(-1.47298996684891,-1.44190071960592,
4.51069454517891));
#17927=CARTESIAN_POINT('Ctrl Pts',(-1.88579546760224,-0.832197441721883,
4.47365729027695));
#17928=CARTESIAN_POINT('Ctrl Pts',(-1.94809599212019,-0.188566869504432,
4.43662003537499));
#17929=CARTESIAN_POINT('Ctrl Pts',(-1.95412372487237,-0.126293989613301,
4.43303658762474));
#17930=CARTESIAN_POINT('Ctrl Pts',(-1.95687036296404,-0.0637035146184469,
4.42945313987448));
#17931=CARTESIAN_POINT('Ctrl Pts',(-1.95645531603829,-0.0010761721163155,
4.42586969212423));
#17932=CARTESIAN_POINT('Ctrl Pts',(-1.95619906720822,-0.0012405029508829,
4.32413030787576));
#17933=CARTESIAN_POINT('Ctrl Pts',(-1.95674893362639,-0.0755294225214843,
4.32837955087737));
#17934=CARTESIAN_POINT('Ctrl Pts',(-1.95288420038623,-0.149760580973872,
4.33262879387898));
#17935=CARTESIAN_POINT('Ctrl Pts',(-1.94441398713267,-0.223462453035597,
4.33687803688058));
#17936=CARTESIAN_POINT('Ctrl Pts',(-1.87052595092818,-0.866384470251901,
4.37394537052913));
#17937=CARTESIAN_POINT('Ctrl Pts',(-1.44618113927919,-1.4690301207881,4.41101270417768));
#17938=CARTESIAN_POINT('Ctrl Pts',(-0.86578855785897,-1.75530378976244,
4.44808003782624));
#17939=CARTESIAN_POINT('Ctrl Pts',(-0.285395976438753,-2.04157745873679,
4.48514737147479));
#17940=CARTESIAN_POINT('Ctrl Pts',(0.451044374752689,-2.01147914614929,
4.52221470512334));
#17941=CARTESIAN_POINT('Ctrl Pts',(1.00614027956814,-1.67879806978219,4.55928203877189));
#17942=CARTESIAN_POINT('Ctrl Pts',(1.56123618438359,-1.34611699341509,4.59634937242044));
#17943=CARTESIAN_POINT('Ctrl Pts',(1.93498764282306,-0.710853153268378,
4.633416706069));
#17944=CARTESIAN_POINT('Ctrl Pts',(1.95616444914465,-0.0640458365273947,
4.67048403971755));
#17945=CARTESIAN_POINT('Ctrl Pts',(1.97734125546624,0.582761480213589,4.7075513733661));
#17946=CARTESIAN_POINT('Ctrl Pts',(1.64594340966995,1.24111227354885,4.74461870701465));
#17947=CARTESIAN_POINT('Ctrl Pts',(1.1137972659727,1.60939021731388,4.7816860406632));
#17948=CARTESIAN_POINT('Ctrl Pts',(0.58165112227545,1.97766816107891,4.81875337431176));
#17949=CARTESIAN_POINT('Ctrl Pts',(-0.151243319322761,2.05587325527372,
4.85582070796031));
#17950=CARTESIAN_POINT('Ctrl Pts',(-0.74911836296885,1.80817667818627,4.89288804160886));
#17951=CARTESIAN_POINT('Ctrl Pts',(-1.34699340661495,1.56048010109882,4.92995537525741));
#17952=CARTESIAN_POINT('Ctrl Pts',(-1.80984905230891,0.986881852729116,
4.96702270890596));
#17953=CARTESIAN_POINT('Ctrl Pts',(-1.92563297048424,0.350169793468709,
5.00409004255452));
#17954=CARTESIAN_POINT('Ctrl Pts',(-1.94649896588392,0.235424748484748,
5.01077013099493));
#17955=CARTESIAN_POINT('Ctrl Pts',(-1.95609296160575,0.118629928772321,
5.01745021943535));
#17956=CARTESIAN_POINT('Ctrl Pts',(-1.95503514488101,0.00166188402949293,
5.02413030787576));
#17957=CARTESIAN_POINT('Origin',(0.,0.,0.));
#17958=CARTESIAN_POINT('',(-1.95079798926752,-3.39345409606611E-5,5.82586969212423));
#17959=CARTESIAN_POINT('',(-1.95081926285686,0.000266806291091909,5.72413030787576));
#17960=CARTESIAN_POINT('',(-1.954,-2.39295984553393E-16,0.));
#17961=CARTESIAN_POINT('Ctrl Pts',(-1.95079827866809,-3.39314739267183E-5,
5.82586969212423));
#17962=CARTESIAN_POINT('Ctrl Pts',(-1.95074743468102,0.328084477385078,
5.80723353203135));
#17963=CARTESIAN_POINT('Ctrl Pts',(-1.87239681557632,0.656225698195148,
5.78859737193847));
#17964=CARTESIAN_POINT('Ctrl Pts',(-1.71588222891389,0.941479492766077,
5.76996121184558));
#17965=CARTESIAN_POINT('Ctrl Pts',(-1.4048272361901,1.50838906258186,5.73292395694362));
#17966=CARTESIAN_POINT('Ctrl Pts',(-0.785047590103655,1.90590592866216,
5.69588670204165));
#17967=CARTESIAN_POINT('Ctrl Pts',(-0.140066859714564,1.95218255642174,
5.65884944713969));
#17968=CARTESIAN_POINT('Ctrl Pts',(0.504913870674523,1.99845918418131,5.62181219223773));
#17969=CARTESIAN_POINT('Ctrl Pts',(1.17509568536624,1.69349557362016,5.58477493733578));
#17970=CARTESIAN_POINT('Ctrl Pts',(1.5638981065899,1.17679997067967,5.54773768243382));
#17971=CARTESIAN_POINT('Ctrl Pts',(1.95270052781355,0.660104367739175,5.51070042753186));
#17972=CARTESIAN_POINT('Ctrl Pts',(2.06012355556913,-0.0683232275806662,
5.47366317262989));
#17973=CARTESIAN_POINT('Ctrl Pts',(1.83702559506323,-0.675257300496502,
5.43662591772793));
#17974=CARTESIAN_POINT('Ctrl Pts',(1.61392763455733,-1.28219137341235,5.39958866282597));
#17975=CARTESIAN_POINT('Ctrl Pts',(1.06030868578995,-1.76763192392419,5.36255140792401));
#17976=CARTESIAN_POINT('Ctrl Pts',(0.429426533588159,-1.90950996620586,
5.32551415302205));
#17977=CARTESIAN_POINT('Ctrl Pts',(-0.201455618613625,-2.05138800848752,
5.28847689812009));
#17978=CARTESIAN_POINT('Ctrl Pts',(-0.909600974249807,-1.84970354253902,
5.25143964321813));
#17979=CARTESIAN_POINT('Ctrl Pts',(-1.37106230481287,-1.39671887475983,
5.21440238831617));
#17980=CARTESIAN_POINT('Ctrl Pts',(-1.73874988399236,-1.03578541214894,
5.18489148958552));
#17981=CARTESIAN_POINT('Ctrl Pts',(-1.94982428002672,-0.515308077485324,
5.15538059085487));
#17982=CARTESIAN_POINT('Ctrl Pts',(-1.95458379985314,0.00173431571939442,
5.12586969212423));
#17983=CARTESIAN_POINT('Ctrl Pts',(-1.95503514488101,0.00166188402949293,
5.02413030787576));
#17984=CARTESIAN_POINT('Ctrl Pts',(-1.95022321215187,-0.530417397378261,
5.0545175530839));
#17985=CARTESIAN_POINT('Ctrl Pts',(-1.72499597458382,-1.06608118124287,
5.08490479829204));
#17986=CARTESIAN_POINT('Ctrl Pts',(-1.33773156155863,-1.42869013102344,
5.11529204350017));
#17987=CARTESIAN_POINT('Ctrl Pts',(-0.86533404380103,-1.87101212610407,
5.15235937714873));
#17988=CARTESIAN_POINT('Ctrl Pts',(-0.151826817629148,-2.05583024611426,
5.18942671079728));
#17989=CARTESIAN_POINT('Ctrl Pts',(0.475904465069911,-1.8984720596839,5.22649404444583));
#17990=CARTESIAN_POINT('Ctrl Pts',(1.10363574776897,-1.74111387325355,5.26356137809438));
#17991=CARTESIAN_POINT('Ctrl Pts',(1.6455910869952,-1.24157938038265,5.30062871174293));
#17992=CARTESIAN_POINT('Ctrl Pts',(1.85347948041758,-0.628724929476167,
5.33769604539148));
#17993=CARTESIAN_POINT('Ctrl Pts',(2.06136787383997,-0.015870478569668,
5.37476337904004));
#17994=CARTESIAN_POINT('Ctrl Pts',(1.93518932145849,0.710303930372423,5.41183071268859));
#17995=CARTESIAN_POINT('Ctrl Pts',(1.53275116822559,1.21710931209029,5.44889804633714));
#17996=CARTESIAN_POINT('Ctrl Pts',(1.13031301499269,1.72391469380815,5.48596537998569));
#17997=CARTESIAN_POINT('Ctrl Pts',(0.451615260908389,2.01135104830178,5.52303271363424));
#17998=CARTESIAN_POINT('Ctrl Pts',(-0.192404026912741,1.94773250517156,
5.56010004728279));
#17999=CARTESIAN_POINT('Ctrl Pts',(-0.836423314733875,1.88411396204135,
5.59716738093134));
#18000=CARTESIAN_POINT('Ctrl Pts',(-1.44576413629184,1.46944052128728,5.6342347145799));
#18001=CARTESIAN_POINT('Ctrl Pts',(-1.74126355620191,0.893690354158911,
5.67130204822845));
#18002=CARTESIAN_POINT('Ctrl Pts',(-1.88164520354535,0.620171181280857,
5.68891146811089));
#18003=CARTESIAN_POINT('Ctrl Pts',(-1.95119678622385,0.310299013274676,
5.70652088799333));
#18004=CARTESIAN_POINT('Ctrl Pts',(-1.95081926285686,0.000266806291091909,
5.72413030787576));
#18005=CARTESIAN_POINT('Origin',(0.,0.,0.));
#18006=CARTESIAN_POINT('',(-1.95470825951396,-0.00171604386803359,6.52586969212423));
#18007=CARTESIAN_POINT('',(-1.954054516794,-0.00178804188155213,6.42413030787577));
#18008=CARTESIAN_POINT('',(-1.954,-2.39295984553393E-16,0.));
#18009=CARTESIAN_POINT('Ctrl Pts',(-1.95470825951396,-0.00171604386803359,
6.52586969212423));
#18010=CARTESIAN_POINT('Ctrl Pts',(-1.94992854745838,0.51935938865238,6.49612372810978));
#18011=CARTESIAN_POINT('Ctrl Pts',(-1.73510566406059,1.04391419457857,6.46637776409532));
#18012=CARTESIAN_POINT('Ctrl Pts',(-1.36219391366738,1.40536941793186,6.43663180008087));
#18013=CARTESIAN_POINT('Ctrl Pts',(-0.897874534119316,1.85542406186529,
6.39959454517891));
#18014=CARTESIAN_POINT('Ctrl Pts',(-0.188466746172986,2.05262208241376,
6.36255729027695));
#18015=CARTESIAN_POINT('Ctrl Pts',(0.441504710548841,1.90675353660593,6.32552003537499));
#18016=CARTESIAN_POINT('Ctrl Pts',(1.07147616727065,1.76088499079811,6.28848278047303));
#18017=CARTESIAN_POINT('Ctrl Pts',(1.62201129276796,1.27194987863399,6.25144552557107));
#18018=CARTESIAN_POINT('Ctrl Pts',(1.84126302416029,0.663615803388951,6.21440827066911));
#18019=CARTESIAN_POINT('Ctrl Pts',(2.06051475555262,0.0552817281439051,
6.17737101576715));
#18020=CARTESIAN_POINT('Ctrl Pts',(1.94848309283996,-0.672451310182071,
6.14033376086519));
#18021=CARTESIAN_POINT('Ctrl Pts',(1.55641789066206,-1.18667552789108,6.10329650596323));
#18022=CARTESIAN_POINT('Ctrl Pts',(1.16435268848415,-1.7008997456001,6.06625925106126));
#18023=CARTESIAN_POINT('Ctrl Pts',(0.492253946840989,-2.00161514269215,
6.02922199615931));
#18024=CARTESIAN_POINT('Ctrl Pts',(-0.152420941573553,-1.95125685529952,
5.99218474125735));
#18025=CARTESIAN_POINT('Ctrl Pts',(-0.79709582998809,-1.90089856790688,
5.95514748635538));
#18026=CARTESIAN_POINT('Ctrl Pts',(-1.41434686517401,-1.49946659602955,
5.91811023145342));
#18027=CARTESIAN_POINT('Ctrl Pts',(-1.7218072130864,-0.930599473315251,
5.88107297655146));
#18028=CARTESIAN_POINT('Ctrl Pts',(-1.8745617038537,-0.647971133646427,
5.86267188174238));
#18029=CARTESIAN_POINT('Ctrl Pts',(-1.95084848133978,-0.324013652614182,
5.84427078693331));
#18030=CARTESIAN_POINT('Ctrl Pts',(-1.95079827866809,-3.39314739267183E-5,
5.82586969212423));
#18031=CARTESIAN_POINT('Ctrl Pts',(-1.95081926285686,0.000266806291091909,
5.72413030787576));
#18032=CARTESIAN_POINT('Ctrl Pts',(-1.95040211015287,-0.342310063843146,
5.74358822164188));
#18033=CARTESIAN_POINT('Ctrl Pts',(-1.86460411668041,-0.685082335623694,
5.76304613540799));
#18034=CARTESIAN_POINT('Ctrl Pts',(-1.69464079239607,-0.979221020005547,
5.78250404917411));
#18035=CARTESIAN_POINT('Ctrl Pts',(-1.37086059041801,-1.53955533353895,
5.81957138282266));
#18036=CARTESIAN_POINT('Ctrl Pts',(-0.741642168199709,-1.92339706710309,
5.85663871647121));
#18037=CARTESIAN_POINT('Ctrl Pts',(-0.0952551698061251,-1.95489326406863,
5.89370605011977));
#18038=CARTESIAN_POINT('Ctrl Pts',(0.551131828587468,-1.98638946103417,
5.93077338376832));
#18039=CARTESIAN_POINT('Ctrl Pts',(1.21468740315634,-1.6655401214011,5.96784071741687));
#18040=CARTESIAN_POINT('Ctrl Pts',(1.59141071326467,-1.1393389148879,6.00490805106542));
#18041=CARTESIAN_POINT('Ctrl Pts',(1.96813402337299,-0.613137708374708,
6.04197538471397));
#18042=CARTESIAN_POINT('Ctrl Pts',(2.05802506902077,0.118415365018621,6.07904271836252));
#18043=CARTESIAN_POINT('Ctrl Pts',(1.81990123568346,0.720167142842566,6.11611005201108));
#18044=CARTESIAN_POINT('Ctrl Pts',(1.58177740234616,1.32191892066651,6.15317738565963));
#18045=CARTESIAN_POINT('Ctrl Pts',(1.01563869002379,1.79386940292107,6.19024471930818));
#18046=CARTESIAN_POINT('Ctrl Pts',(0.380855453001195,1.91979955860115,6.22731205295673));
#18047=CARTESIAN_POINT('Ctrl Pts',(-0.253927784021398,2.04572971428122,
6.26437938660528));
#18048=CARTESIAN_POINT('Ctrl Pts',(-0.957355545744209,1.82563954338681,
6.30144672025383));
#18049=CARTESIAN_POINT('Ctrl Pts',(-1.40715997837402,1.36036098757553,6.33851405390239));
#18050=CARTESIAN_POINT('Ctrl Pts',(-1.75347182721572,1.0021353561665,6.36705280522685));
#18051=CARTESIAN_POINT('Ctrl Pts',(-1.94944302076728,0.498569063116626,
6.39559155655131));
#18052=CARTESIAN_POINT('Ctrl Pts',(-1.954054516794,-0.00178804188155213,
6.42413030787577));
#18053=CARTESIAN_POINT('Origin',(0.,0.,0.));
#18054=CARTESIAN_POINT('',(-1.95636485901942,0.00113456228253272,7.22586969212423));
#18055=CARTESIAN_POINT('',(-1.95685604123946,0.000756211846537467,7.12413030787577));
#18056=CARTESIAN_POINT('',(-1.954,-2.39295984553393E-16,0.));
#18057=CARTESIAN_POINT('Ctrl Pts',(-1.95636485901942,0.00113456228253272,
7.22586969212423));
#18058=CARTESIAN_POINT('Ctrl Pts',(-1.95682612605948,0.0678782264229027,
7.22205117909017));
#18059=CARTESIAN_POINT('Ctrl Pts',(-1.95370640484,0.134578270129128,7.21823266605611));
#18060=CARTESIAN_POINT('Ctrl Pts',(-1.94686336470326,0.200894109800786,
7.21441415302205));
#18061=CARTESIAN_POINT('Ctrl Pts',(-1.88049003571683,0.844117436799507,
7.17737689812009));
#18062=CARTESIAN_POINT('Ctrl Pts',(-1.46383354330961,1.45119553755835,7.14033964321813));
#18063=CARTESIAN_POINT('Ctrl Pts',(-0.887496963111741,1.7444152651618,7.10330238831617));
#18064=CARTESIAN_POINT('Ctrl Pts',(-0.311160382913887,2.03763499276525,
7.0662651334142));
#18065=CARTESIAN_POINT('Ctrl Pts',(0.42485628507463,2.01699634721332,7.02922787851224));
#18066=CARTESIAN_POINT('Ctrl Pts',(0.983855814420553,1.6919406608931,6.99219062361028));
#18067=CARTESIAN_POINT('Ctrl Pts',(1.5428553437665,1.36688497457287,6.95515336870832));
#18068=CARTESIAN_POINT('Ctrl Pts',(1.92483773446985,0.737412247484355,6.91811611380636));
#18069=CARTESIAN_POINT('Ctrl Pts',(1.95506184522045,0.0914802298548023,
6.8810788589044));
#18070=CARTESIAN_POINT('Ctrl Pts',(1.98528595597105,-0.554451787774746,
6.84404160400244));
#18071=CARTESIAN_POINT('Ctrl Pts',(1.66375178676889,-1.21684309594531,6.80700434910048));
#18072=CARTESIAN_POINT('Ctrl Pts',(1.13754792239338,-1.59267705016464,6.76996709419852));
#18073=CARTESIAN_POINT('Ctrl Pts',(0.611344058017871,-1.96851100438396,
6.73292983929656));
#18074=CARTESIAN_POINT('Ctrl Pts',(-0.119529501530993,-2.05778760465205,
6.69589258439459));
#18075=CARTESIAN_POINT('Ctrl Pts',(-0.72072831037795,-1.81966649740579,
6.65885532949263));
#18076=CARTESIAN_POINT('Ctrl Pts',(-1.3219271192249,-1.58154539015953,6.62181807459067));
#18077=CARTESIAN_POINT('Ctrl Pts',(-1.79345117736996,-1.01602657539894,
6.58478081968872));
#18078=CARTESIAN_POINT('Ctrl Pts',(-1.91959772086759,-0.381811534359454,
6.54774356478676));
#18079=CARTESIAN_POINT('Ctrl Pts',(-1.94443139565072,-0.256957617359055,
6.54045227389925));
#18080=CARTESIAN_POINT('Ctrl Pts',(-1.95587985613591,-0.129441356485054,
6.53316098301174));
#18081=CARTESIAN_POINT('Ctrl Pts',(-1.95470825951396,-0.00171604386803359,
6.52586969212423));
#18082=CARTESIAN_POINT('Ctrl Pts',(-1.954054516794,-0.00178804188155213,
6.42413030787577));
#18083=CARTESIAN_POINT('Ctrl Pts',(-1.95543262626536,-0.151315844023487,
6.43265889019986));
#18084=CARTESIAN_POINT('Ctrl Pts',(-1.93972104383109,-0.300557044358562,
6.44118747252395));
#18085=CARTESIAN_POINT('Ctrl Pts',(-1.90582502907504,-0.445547056796695,
6.44971605484804));
#18086=CARTESIAN_POINT('Ctrl Pts',(-1.75850454360942,-1.07570960462949,
6.4867833884966));
#18087=CARTESIAN_POINT('Ctrl Pts',(-1.26768246914137,-1.62556775956693,
6.52385072214515));
#18088=CARTESIAN_POINT('Ctrl Pts',(-0.658223653418358,-1.84320992928983,
6.5609180557937));
#18089=CARTESIAN_POINT('Ctrl Pts',(-0.0487648376953535,-2.06085209901273,
6.59798538944225));
#18090=CARTESIAN_POINT('Ctrl Pts',(0.679330719282597,-1.94627828352109,
6.63505272309081));
#18091=CARTESIAN_POINT('Ctrl Pts',(1.19249387898998,-1.55197924267736,6.67212005673936));
#18092=CARTESIAN_POINT('Ctrl Pts',(1.70565703869737,-1.15768020183362,6.70918739038791));
#18093=CARTESIAN_POINT('Ctrl Pts',(2.00388780113418,-0.483655935637787,
6.74625472403646));
#18094=CARTESIAN_POINT('Ctrl Pts',(1.95055495411266,0.161296597217467,6.78332205768501));
#18095=CARTESIAN_POINT('Ctrl Pts',(1.89722210709115,0.806249130072731,6.82038939133356));
#18096=CARTESIAN_POINT('Ctrl Pts',(1.49232565061129,1.42212992958742,6.85745672498212));
#18097=CARTESIAN_POINT('Ctrl Pts',(0.921364535931439,1.72677983938191,6.89452405863067));
#18098=CARTESIAN_POINT('Ctrl Pts',(0.35040342125159,2.03142974917639,6.93159139227922));
#18099=CARTESIAN_POINT('Ctrl Pts',(-0.386622351628245,2.02484876925069,
6.96865872592777));
#18100=CARTESIAN_POINT('Ctrl Pts',(-0.95205236204405,1.7100519056834,7.00572605957632));
#18101=CARTESIAN_POINT('Ctrl Pts',(-1.51748237245986,1.39525504211611,7.04279339322487));
#18102=CARTESIAN_POINT('Ctrl Pts',(-1.91131662041163,0.772242294907221,
7.07986072687343));
#18103=CARTESIAN_POINT('Ctrl Pts',(-1.95312418617604,0.126440243047374,
7.11692806052198));
#18104=CARTESIAN_POINT('Ctrl Pts',(-1.95583194707364,0.0846134226707359,
7.11932880963991));
#18105=CARTESIAN_POINT('Ctrl Pts',(-1.95706302779737,0.0426910058065101,
7.12172955875784));
#18106=CARTESIAN_POINT('Ctrl Pts',(-1.95685604123946,0.000756211846537467,
7.12413030787577));
#18107=CARTESIAN_POINT('Origin',(0.,0.,0.));
#18108=CARTESIAN_POINT('',(-1.95128693461656,0.000980964721550987,7.92586969212423));
#18109=CARTESIAN_POINT('',(-1.95179084094767,0.00133979406531506,7.82413030787577));
#18110=CARTESIAN_POINT('',(-1.954,-2.39295984553393E-16,0.));
#18111=CARTESIAN_POINT('Ctrl Pts',(-1.95128693461656,0.000980964721550987,
7.92586969212423));
#18112=CARTESIAN_POINT('Ctrl Pts',(-1.95248078249778,0.263652730728045,
7.9109413751686));
#18113=CARTESIAN_POINT('Ctrl Pts',(-1.90315517629326,0.525894534188289,
7.89601305821297));
#18114=CARTESIAN_POINT('Ctrl Pts',(-1.80118142285547,0.765753467326086,
7.88108474125734));
#18115=CARTESIAN_POINT('Ctrl Pts',(-1.54818385383207,1.36084509577563,7.84404748635538));
#18116=CARTESIAN_POINT('Ctrl Pts',(-0.971116173277759,1.81816132921196,
7.80701023145342));
#18117=CARTESIAN_POINT('Ctrl Pts',(-0.333960757905731,1.9284984258719,7.76997297655146));
#18118=CARTESIAN_POINT('Ctrl Pts',(0.303194657466307,2.03883552253184,7.7329357216495));
#18119=CARTESIAN_POINT('Ctrl Pts',(1.00043780765606,1.80219348241539,7.69589846674754));
#18120=CARTESIAN_POINT('Ctrl Pts',(1.43880759949705,1.3268265031207,7.65886121184558));
#18121=CARTESIAN_POINT('Ctrl Pts',(1.87717739133805,0.851459523826022,7.62182395694362));
#18122=CARTESIAN_POINT('Ctrl Pts',(2.05667382483028,0.137367605353111,7.58478670204165));
#18123=CARTESIAN_POINT('Ctrl Pts',(1.8951853172685,-0.488781846291726,7.54774944713969));
#18124=CARTESIAN_POINT('Ctrl Pts',(1.73369680970672,-1.11493129793655,7.51071219223773));
#18125=CARTESIAN_POINT('Ctrl Pts',(1.23122336109093,-1.65313828275331,7.47367493733578));
#18126=CARTESIAN_POINT('Ctrl Pts',(0.617625480567028,-1.85719528451254,
7.43663768243382));
#18127=CARTESIAN_POINT('Ctrl Pts',(0.00402760004311595,-2.06125228627176,
7.39960042753186));
#18128=CARTESIAN_POINT('Ctrl Pts',(-0.720694712388916,-1.93115930497345,
7.36256317262989));
#18129=CARTESIAN_POINT('Ctrl Pts',(-1.22501078582212,-1.52642853770499,
7.32552591772793));
#18130=CARTESIAN_POINT('Ctrl Pts',(-1.67733225261428,-1.16342520715373,
7.29230717586003));
#18131=CARTESIAN_POINT('Ctrl Pts',(-1.95235211620587,-0.579494737819326,
7.25908843399213));
#18132=CARTESIAN_POINT('Ctrl Pts',(-1.95636485901942,0.00113456228253272,
7.22586969212423));
#18133=CARTESIAN_POINT('Ctrl Pts',(-1.95685604123946,0.000756211846537467,
7.12413030787577));
#18134=CARTESIAN_POINT('Ctrl Pts',(-1.95386717540877,-0.604778147712892,
7.15879689240639));
#18135=CARTESIAN_POINT('Ctrl Pts',(-1.65102574974132,-1.21289326541241,
7.19346347693701));
#18136=CARTESIAN_POINT('Ctrl Pts',(-1.16459038479062,-1.57302589296855,
7.22813006146763));
#18137=CARTESIAN_POINT('Ctrl Pts',(-0.644468134063717,-1.95809862061383,
7.26519739511619));
#18138=CARTESIAN_POINT('Ctrl Pts',(0.0855572509671633,-2.05965271939359,
7.30226472876474));
#18139=CARTESIAN_POINT('Ctrl Pts',(0.691032502683693,-1.83116227947434,
7.33933206241329));
#18140=CARTESIAN_POINT('Ctrl Pts',(1.29650775440023,-1.60267183955508,7.37639939606184));
#18141=CARTESIAN_POINT('Ctrl Pts',(1.7774328728024,-1.0441368609368,7.41346672971039));
#18142=CARTESIAN_POINT('Ctrl Pts',(1.91347719234508,-0.411444116083022,
7.45053406335894));
#18143=CARTESIAN_POINT('Ctrl Pts',(2.04952151188775,0.221248628770744,7.4876013970075));
#18144=CARTESIAN_POINT('Ctrl Pts',(1.84068503257092,0.928099139860014,7.52466873065605));
#18145=CARTESIAN_POINT('Ctrl Pts',(1.38264394156525,1.38527144266209,7.5617360643046));
#18146=CARTESIAN_POINT('Ctrl Pts',(0.924602850559573,1.84244374546417,7.59880339795316));
#18147=CARTESIAN_POINT('Ctrl Pts',(0.21735714786506,2.04993783997907,7.63587073160171));
#18148=CARTESIAN_POINT('Ctrl Pts',(-0.415076170159516,1.9126925888594,7.67293806525026));
#18149=CARTESIAN_POINT('Ctrl Pts',(-1.0475094881841,1.77544733773972,7.71000539889881));
#18150=CARTESIAN_POINT('Ctrl Pts',(-1.60513042153874,1.29346274098546,7.74707273254736));
#18151=CARTESIAN_POINT('Ctrl Pts',(-1.83247093326142,0.687554760545781,
7.78414006619591));
#18152=CARTESIAN_POINT('Ctrl Pts',(-1.91422667443603,0.469659341691089,
7.79747014675586));
#18153=CARTESIAN_POINT('Ctrl Pts',(-1.95326886402229,0.235737517711039,
7.81080022731581));
#18154=CARTESIAN_POINT('Ctrl Pts',(-1.95179084094767,0.00133979406531506,
7.82413030787577));
#18155=CARTESIAN_POINT('Origin',(0.,0.,0.));
#18156=CARTESIAN_POINT('',(-1.95285709583883,-0.00166548583676096,8.62586969212423));
#18157=CARTESIAN_POINT('',(-1.95199070173634,-0.00143915622514865,8.52413030787577));
#18158=CARTESIAN_POINT('',(-1.954,-2.39295984553393E-16,0.));
#18159=CARTESIAN_POINT('Ctrl Pts',(-1.95285709583883,-0.00166548583676096,
8.62586969212423));
#18160=CARTESIAN_POINT('Ctrl Pts',(-1.94908690947408,0.455599167126523,
8.59983157124703));
#18161=CARTESIAN_POINT('Ctrl Pts',(-1.78874742560419,0.915224010975134,
8.57379345036984));
#18162=CARTESIAN_POINT('Ctrl Pts',(-1.49546401894218,1.26258187482945,8.54775532949264));
#18163=CARTESIAN_POINT('Ctrl Pts',(-1.07829058533359,1.75667212836379,8.51071807459068));
#18164=CARTESIAN_POINT('Ctrl Pts',(-0.392132937906689,2.02361363589085,
8.47368081968872));
#18165=CARTESIAN_POINT('Ctrl Pts',(0.249226660225596,1.94126935410646,8.43664356478675));
#18166=CARTESIAN_POINT('Ctrl Pts',(0.890586258357889,1.85892507232208,8.39960630988479));
#18167=CARTESIAN_POINT('Ctrl Pts',(1.48714780719556,1.42729500122627,8.36256905498283));
#18168=CARTESIAN_POINT('Ctrl Pts',(1.76595313409068,0.84384378564397,8.32553180008087));
#18169=CARTESIAN_POINT('Ctrl Pts',(2.04475846098579,0.260392570061681,8.28849454517891));
#18170=CARTESIAN_POINT('Ctrl Pts',(2.00580756593834,-0.474879790007082,
8.25145729027695));
#18171=CARTESIAN_POINT('Ctrl Pts',(1.66694824118237,-1.02562274217559,8.21442003537499));
#18172=CARTESIAN_POINT('Ctrl Pts',(1.3280889164264,-1.5763656943441,8.17738278047303));
#18173=CARTESIAN_POINT('Ctrl Pts',(0.689321161961899,-1.94257923861236,
8.14034552557107));
#18174=CARTESIAN_POINT('Ctrl Pts',(0.0428393990027941,-1.95673258160789,
8.10330827066911));
#18175=CARTESIAN_POINT('Ctrl Pts',(-0.60364236395632,-1.97088592460343,
8.06627101576715));
#18176=CARTESIAN_POINT('Ctrl Pts',(-1.25783813541006,-1.63297906632622,
8.02923376086519));
#18177=CARTESIAN_POINT('Ctrl Pts',(-1.62047229239069,-1.09759212545623,
7.99219650596323));
#18178=CARTESIAN_POINT('Ctrl Pts',(-1.83694233303294,-0.777999415783143,
7.9700875680169));
#18179=CARTESIAN_POINT('Ctrl Pts',(-1.94951883786448,-0.388037689702213,
7.94797863007056));
#18180=CARTESIAN_POINT('Ctrl Pts',(-1.95128693461656,0.000980964721550987,
7.92586969212423));
#18181=CARTESIAN_POINT('Ctrl Pts',(-1.95179084094767,0.00133979406531506,
7.82413030787577));
#18182=CARTESIAN_POINT('Ctrl Pts',(-1.94915888327607,-0.416058890402282,
7.84786756096437));
#18183=CARTESIAN_POINT('Ctrl Pts',(-1.81803758852289,-0.834966649688199,
7.87160481405297));
#18184=CARTESIAN_POINT('Ctrl Pts',(-1.57081203637628,-1.16757477949376,
7.89534206714157));
#18185=CARTESIAN_POINT('Ctrl Pts',(-1.18475253767773,-1.68696497496857,
7.93240940079012));
#18186=CARTESIAN_POINT('Ctrl Pts',(-0.5155734501899,-1.99591400179311,7.96947673443867));
#18187=CARTESIAN_POINT('Ctrl Pts',(0.130148074857978,-1.95288051881755,
8.00654406808722));
#18188=CARTESIAN_POINT('Ctrl Pts',(0.775869599905848,-1.90984703584199,
8.04361140173578));
#18189=CARTESIAN_POINT('Ctrl Pts',(1.39813356251376,-1.51483104306634,8.08067873538433));
#18190=CARTESIAN_POINT('Ctrl Pts',(1.71185635075732,-0.948804238199317,
8.11774606903288));
#18191=CARTESIAN_POINT('Ctrl Pts',(2.02557913900088,-0.382777433332289,
8.15481340268144));
#18192=CARTESIAN_POINT('Ctrl Pts',(2.03076075288008,0.354260183626113,8.19188073632998));
#18193=CARTESIAN_POINT('Ctrl Pts',(1.72502744155934,0.924641574518184,8.22894806997854));
#18194=CARTESIAN_POINT('Ctrl Pts',(1.41929413023861,1.49502296541025,8.26601540362709));
#18195=CARTESIAN_POINT('Ctrl Pts',(0.80264589371795,1.89874813023598,8.30308273727564));
#18196=CARTESIAN_POINT('Ctrl Pts',(0.157593195636322,1.9508570009308,8.3401500709242));
#18197=CARTESIAN_POINT('Ctrl Pts',(-0.487459502445315,2.00296587162561,
8.37721740457275));
#18198=CARTESIAN_POINT('Ctrl Pts',(-1.16091666208792,1.7034584481895,8.4142847382213));
#18199=CARTESIAN_POINT('Ctrl Pts',(-1.55424059489758,1.18954651103718,8.45135207186985));
#18200=CARTESIAN_POINT('Ctrl Pts',(-1.81165882267556,0.853207201220195,
8.47561148387182));
#18201=CARTESIAN_POINT('Ctrl Pts',(-1.94908776418844,0.42503214287857,8.4998708958738));
#18202=CARTESIAN_POINT('Ctrl Pts',(-1.95199070173634,-0.00143915622514865,
8.52413030787577));
#18203=CARTESIAN_POINT('Origin',(0.,0.,-1.2940562256037));
#18204=CARTESIAN_POINT('',(-1.55459018043874,-0.0013258255983764,8.8559437743963));
#18205=CARTESIAN_POINT('',(-1.55786620250461,-0.000579511545185651,8.99405622560371));
#18206=CARTESIAN_POINT('',(-1.5555,-1.46451138874614E-13,-1.2940562256037));
#18207=CARTESIAN_POINT('',(-0.840025297123077,1.30917445368953,9.44449999999999));
#18208=CARTESIAN_POINT('Ctrl Pts',(-1.55459018043874,-0.00132582559837632,
8.8559437743963));
#18209=CARTESIAN_POINT('Ctrl Pts',(-1.55585799906995,-0.155092401130408,
8.86694290842106));
#18210=CARTESIAN_POINT('Ctrl Pts',(-1.46426308580118,-0.825171155750169,
8.91497929734778));
#18211=CARTESIAN_POINT('Ctrl Pts',(-0.502885372776985,-1.76823019847661,
9.00005294117646));
#18212=CARTESIAN_POINT('Ctrl Pts',(1.21162302759592,-1.38188780683742,9.11116470588235));
#18213=CARTESIAN_POINT('Ctrl Pts',(1.81992793219366,0.268272986849182,9.22227647058824));
#18214=CARTESIAN_POINT('Ctrl Pts',(0.758516013178858,1.6740067592164,9.33338823529411));
#18215=CARTESIAN_POINT('Ctrl Pts',(-0.404795980777633,1.58843718658925,
9.40746274509804));
#18216=CARTESIAN_POINT('Ctrl Pts',(-0.840025297123196,1.30917445368946,
9.4445));
#18217=CARTESIAN_POINT('',(0.964986447796937,1.21999237930745,9.44449999999999));
#18218=CARTESIAN_POINT('Origin',(0.,0.,9.4445));
#18219=CARTESIAN_POINT('Ctrl Pts',(-1.55786620250461,-0.000579511545185591,
8.99405622560371));
#18220=CARTESIAN_POINT('Ctrl Pts',(-1.55797190598053,-0.026693910339596,
8.99593481580826));
#18221=CARTESIAN_POINT('Ctrl Pts',(-1.54554514373521,-0.567968451132823,
9.03488073966137));
#18222=CARTESIAN_POINT('Ctrl Pts',(-0.917075781704608,-1.59325581253419,
9.11089399716304));
#18223=CARTESIAN_POINT('Ctrl Pts',(0.84291969341562,-1.63568507599433,9.22209599810868));
#18224=CARTESIAN_POINT('Ctrl Pts',(1.83002015964776,-0.174643446395858,
9.33329799905435));
#18225=CARTESIAN_POINT('Ctrl Pts',(1.37089695500413,0.898926325849287,9.40743266635145));
#18226=CARTESIAN_POINT('Ctrl Pts',(0.964986447796868,1.2199923793075,9.4445));
#18227=CARTESIAN_POINT('Origin',(0.,0.,-1.2940562256037));
#18228=CARTESIAN_POINT('',(-1.55334023889256,0.000780906153647187,8.1559437743963));
#18229=CARTESIAN_POINT('',(-1.55390047929932,-0.00114565379145046,8.29405622560371));
#18230=CARTESIAN_POINT('',(-1.5555,-1.46451138874614E-13,-1.2940562256037));
#18231=CARTESIAN_POINT('Ctrl Pts',(-1.55334023889256,0.000780906153647377,
8.1559437743963));
#18232=CARTESIAN_POINT('Ctrl Pts',(-1.55193272891411,-0.308901037017355,
8.17805271234263));
#18233=CARTESIAN_POINT('Ctrl Pts',(-1.31218630866396,-1.13937563740009,
8.23719890519093));
#18234=CARTESIAN_POINT('Ctrl Pts',(0.0402435134914415,-1.83793611758998,
8.33338235294118));
#18235=CARTESIAN_POINT('Ctrl Pts',(1.56573467327064,-0.963352952631984,
8.44449411764705));
#18236=CARTESIAN_POINT('Ctrl Pts',(1.65875634765081,0.792608392434986,8.55560588235294));
#18237=CARTESIAN_POINT('Ctrl Pts',(0.234061123673802,1.82341787389281,8.66671764705882));
#18238=CARTESIAN_POINT('Ctrl Pts',(-1.24239126631522,1.24902155512614,8.76683027773994));
#18239=CARTESIAN_POINT('Ctrl Pts',(-1.55158888827378,0.362683983861408,
8.8299056535191));
#18240=CARTESIAN_POINT('Ctrl Pts',(-1.55459018043874,-0.00132582559837632,
8.8559437743963));
#18241=CARTESIAN_POINT('Ctrl Pts',(-1.55390047929932,-0.00114565379145014,
8.29405622560371));
#18242=CARTESIAN_POINT('Ctrl Pts',(-1.55512054028755,-0.180385126241298,
8.30686414725028));
#18243=CARTESIAN_POINT('Ctrl Pts',(-1.44363174688106,-0.876888376361596,
8.35673940254541));
#18244=CARTESIAN_POINT('Ctrl Pts',(-0.415210463238687,-1.79137506804378,
8.4436819914891));
#18245=CARTESIAN_POINT('Ctrl Pts',(1.28062367350908,-1.31967978545922,8.55488399243474));
#18246=CARTESIAN_POINT('Ctrl Pts',(1.80303816946195,0.361303122856545,8.66608599338042));
#18247=CARTESIAN_POINT('Ctrl Pts',(0.673390003682997,1.71105376251155,8.77728799432605));
#18248=CARTESIAN_POINT('Ctrl Pts',(-1.04380561312476,1.49701963955364,8.88661140506718));
#18249=CARTESIAN_POINT('Ctrl Pts',(-1.55588622172637,0.488581390679574,
8.95886748215971));
#18250=CARTESIAN_POINT('Ctrl Pts',(-1.55786620250461,-0.000579511545185591,
8.99405622560371));
#18251=CARTESIAN_POINT('Origin',(0.,0.,-1.2940562256037));
#18252=CARTESIAN_POINT('',(-1.55738256817027,0.00090317893057067,7.4559437743963));
#18253=CARTESIAN_POINT('',(-1.55374137824673,0.00106655561326607,7.59405622560371));
#18254=CARTESIAN_POINT('',(-1.5555,-1.46451138874614E-13,-1.2940562256037));
#18255=CARTESIAN_POINT('Ctrl Pts',(-1.55738256817027,0.000903178930570731,
7.4559437743963));
#18256=CARTESIAN_POINT('Ctrl Pts',(-1.55418818667256,-0.461312213243642,
7.4891625162642));
#18257=CARTESIAN_POINT('Ctrl Pts',(-1.09115753827425,-1.44443285152936,
7.55941851303406));
#18258=CARTESIAN_POINT('Ctrl Pts',(0.580128192863429,-1.74444092308354,
7.66671176470588));
#18259=CARTESIAN_POINT('Ctrl Pts',(1.7801242767762,-0.459106790715335,7.77782352941176));
#18260=CARTESIAN_POINT('Ctrl Pts',(1.35145482596167,1.2462718876643,7.88893529411764));
#18261=CARTESIAN_POINT('Ctrl Pts',(-0.313685993055972,1.81141522451351,
8.00004705882353));
#18262=CARTESIAN_POINT('Ctrl Pts',(-1.41760501663887,0.93657834333742,8.08904988558308));
#18263=CARTESIAN_POINT('Ctrl Pts',(-1.55429061267928,0.209883225510418,
8.14101545744067));
#18264=CARTESIAN_POINT('Ctrl Pts',(-1.55334023889256,0.000780906153647377,
8.1559437743963));
#18265=CARTESIAN_POINT('Ctrl Pts',(-1.55374137824673,0.00106655561326607,
7.59405622560371));
#18266=CARTESIAN_POINT('Ctrl Pts',(-1.55164618369287,-0.331207576264562,
7.61779347869231));
#18267=CARTESIAN_POINT('Ctrl Pts',(-1.28426886371588,-1.18542758840111,
7.67859806542946));
#18268=CARTESIAN_POINT('Ctrl Pts',(0.122279206149944,-1.83480779990519,
7.77646998581516));
#18269=CARTESIAN_POINT('Ctrl Pts',(1.6083563717128,-0.891439258304551,7.88767198676082));
#18270=CARTESIAN_POINT('Ctrl Pts',(1.6207309884821,0.868737834600438,7.99887398770647));
#18271=CARTESIAN_POINT('Ctrl Pts',(0.148065176955119,1.83290543012718,8.11007598865213));
#18272=CARTESIAN_POINT('Ctrl Pts',(-1.27502705969297,1.20001188521837,8.20847006795121));
#18273=CARTESIAN_POINT('Ctrl Pts',(-1.55158956867716,0.33835081793624,8.26979681360173));
#18274=CARTESIAN_POINT('Ctrl Pts',(-1.55390047929932,-0.00114565379145014,
8.29405622560371));
#18275=CARTESIAN_POINT('Origin',(0.,0.,-1.2940562256037));
#18276=CARTESIAN_POINT('',(-1.55606381661923,-0.00136607279268914,6.7559437743963));
#18277=CARTESIAN_POINT('',(-1.55777357837665,0.000601989522525624,6.8940562256037));
#18278=CARTESIAN_POINT('',(-1.5555,-1.46451138874614E-13,-1.2940562256037));
#18279=CARTESIAN_POINT('Ctrl Pts',(-1.55606381661923,-0.00136607279268905,
6.7559437743963));
#18280=CARTESIAN_POINT('Ctrl Pts',(-1.5569964770826,-0.103043004100637,
6.76323506528381));
#18281=CARTESIAN_POINT('Ctrl Pts',(-1.50158858796583,-0.720192082985852,
6.80756361107328));
#18282=CARTESIAN_POINT('Ctrl Pts',(-0.676971321141057,-1.70919056845102,
6.8889294117647));
#18283=CARTESIAN_POINT('Ctrl Pts',(1.06848490487467,-1.49598214718639,7.00004117647059));
#18284=CARTESIAN_POINT('Ctrl Pts',(1.83636576494725,0.0859262661083765,
7.11115294117646));
#18285=CARTESIAN_POINT('Ctrl Pts',(0.924123786330422,1.58921924510457,7.22226470588235));
#18286=CARTESIAN_POINT('Ctrl Pts',(-0.833615098607335,1.63850800634715,
7.33337647058823));
#18287=CARTESIAN_POINT('Ctrl Pts',(-1.53117800274423,0.622142797307338,
7.41126949342621));
#18288=CARTESIAN_POINT('Ctrl Pts',(-1.55774976411747,0.0540350978509258,
7.45212526136224));
#18289=CARTESIAN_POINT('Ctrl Pts',(-1.55738256817027,0.000903178930570731,
7.4559437743963));
#18290=CARTESIAN_POINT('Ctrl Pts',(-1.55777357837665,0.000601989522525581,
6.8940562256037));
#18291=CARTESIAN_POINT('Ctrl Pts',(-1.55539426374015,-0.481439308478815,
6.92872281013432));
#18292=CARTESIAN_POINT('Ctrl Pts',(-1.05653937162455,-1.48315563828813,
7.0004567283135));
#18293=CARTESIAN_POINT('Ctrl Pts',(0.649252195647424,-1.72044892818251,
7.10925798014122));
#18294=CARTESIAN_POINT('Ctrl Pts',(1.79778702933405,-0.386567926277561,
7.22045998108688));
#18295=CARTESIAN_POINT('Ctrl Pts',(1.29904832373936,1.30151698160267,7.33166198203254));
#18296=CARTESIAN_POINT('Ctrl Pts',(-0.389980372076409,1.79704983321667,
7.44286398297819));
#18297=CARTESIAN_POINT('Ctrl Pts',(-1.43741330909764,0.891691889173598,
7.53032873083525));
#18298=CARTESIAN_POINT('Ctrl Pts',(-1.55491797235757,0.18766105875093,7.58072614504376));
#18299=CARTESIAN_POINT('Ctrl Pts',(-1.55374137824673,0.00106655561326607,
7.59405622560371));
#18300=CARTESIAN_POINT('Origin',(0.,0.,-1.2940562256037));
#18301=CARTESIAN_POINT('',(-1.55295095520957,-2.70144831846062E-5,6.0559437743963));
#18302=CARTESIAN_POINT('',(-1.55554339860443,-0.00142338748566243,6.19405622560371));
#18303=CARTESIAN_POINT('',(-1.5555,-1.46451138874614E-13,-1.2940562256037));
#18304=CARTESIAN_POINT('Ctrl Pts',(-1.55295123974832,-2.70114676757111E-5,
6.0559437743963));
#18305=CARTESIAN_POINT('Ctrl Pts',(-1.55299120405527,-0.257934102682435,
6.07434486920538));
#18306=CARTESIAN_POINT('Ctrl Pts',(-1.37002901128568,-1.03489667794099,
6.12978321891642));
#18307=CARTESIAN_POINT('Ctrl Pts',(-0.143167133221453,-1.83279178845155,
6.2222588235294));
#18308=CARTESIAN_POINT('Ctrl Pts',(1.46192436006299,-1.11462986392232,6.3333705882353));
#18309=CARTESIAN_POINT('Ctrl Pts',(1.72947592303562,0.623326238098233,6.44448235294117));
#18310=CARTESIAN_POINT('Ctrl Pts',(0.414699995127109,1.79099036343795,6.55559411764706));
#18311=CARTESIAN_POINT('Ctrl Pts',(-1.16831716986105,1.35095029518097,6.65941459146543));
#18312=CARTESIAN_POINT('Ctrl Pts',(-1.55225888207347,0.413440905347305,
6.72619781038185));
#18313=CARTESIAN_POINT('Ctrl Pts',(-1.55606381661923,-0.00136607279268905,
6.7559437743963));
#18314=CARTESIAN_POINT('Ctrl Pts',(-1.55554339860443,-0.00142338748566248,
6.19405622560371));
#18315=CARTESIAN_POINT('Ctrl Pts',(-1.55664045555565,-0.120456394769041,
6.2025848079278));
#18316=CARTESIAN_POINT('Ctrl Pts',(-1.48977304843445,-0.755616611367758,
6.24818072390044));
#18317=CARTESIAN_POINT('Ctrl Pts',(-0.618426992791356,-1.73176817298442,
6.33084397352162));
#18318=CARTESIAN_POINT('Ctrl Pts',(1.12039486833334,-1.45814549642773,6.4420459744673));
#18319=CARTESIAN_POINT('Ctrl Pts',(1.83262304280178,0.151544492417154,6.55324797541294));
#18320=CARTESIAN_POINT('Ctrl Pts',(0.865658194202354,1.62237752769619,6.6644499763586));
#18321=CARTESIAN_POINT('Ctrl Pts',(-0.894490612933678,1.60666097558597,
6.77565197730426));
#18322=CARTESIAN_POINT('Ctrl Pts',(-1.54182702766399,0.582629063158458,
6.85218739371929));
#18323=CARTESIAN_POINT('Ctrl Pts',(-1.55793835196459,0.0339845749906982,
6.89165547648577));
#18324=CARTESIAN_POINT('Ctrl Pts',(-1.55777357837665,0.000601989522525581,
6.8940562256037));
#18325=CARTESIAN_POINT('Origin',(0.,0.,-1.2940562256037));
#18326=CARTESIAN_POINT('',(-1.55596473934061,0.00138061827089577,5.3559437743963));
#18327=CARTESIAN_POINT('',(-1.55296794440831,0.000212393646609743,5.49405622560371));
#18328=CARTESIAN_POINT('',(-1.5555,-1.46451138874614E-13,-1.2940562256037));
#18329=CARTESIAN_POINT('Ctrl Pts',(-1.55596473934061,0.00138061827089576,
5.3559437743963));
#18330=CARTESIAN_POINT('Ctrl Pts',(-1.55217587900794,-0.41021582115075,
5.38545467312695));
#18331=CARTESIAN_POINT('Ctrl Pts',(-1.17326717115581,-1.34454702402952,
5.45200282675955));
#18332=CARTESIAN_POINT('Ctrl Pts',(0.403355110511087,-1.79357944420943,
5.55558823529412));
#18333=CARTESIAN_POINT('Ctrl Pts',(1.72549575760574,-0.634260954463495,
5.6667));
#18334=CARTESIAN_POINT('Ctrl Pts',(1.46895043569095,1.10535387335637,5.77781176470588));
#18335=CARTESIAN_POINT('Ctrl Pts',(-0.131563094636045,1.83366128824048,
5.88892352941177));
#18336=CARTESIAN_POINT('Ctrl Pts',(-1.36658225210923,1.04153952669523,5.98163419930856));
#18337=CARTESIAN_POINT('Ctrl Pts',(-1.55291076491625,0.261174720866106,
6.03730761430341));
#18338=CARTESIAN_POINT('Ctrl Pts',(-1.55295123974832,-2.70114676757111E-5,
6.0559437743963));
#18339=CARTESIAN_POINT('Ctrl Pts',(-1.55296794440831,0.000212393646609865,
5.49405622560371));
#18340=CARTESIAN_POINT('Ctrl Pts',(-1.55263586609147,-0.272499132194598,
5.51351413936982));
#18341=CARTESIAN_POINT('Ctrl Pts',(-1.35422347770915,-1.06517810244381,
5.57003938678448));
#18342=CARTESIAN_POINT('Ctrl Pts',(-0.089495975882287,-1.83669905549533,
5.66363196784771));
#18343=CARTESIAN_POINT('Ctrl Pts',(1.49519291292304,-1.07045369039924,5.77483396879335));
#18344=CARTESIAN_POINT('Ctrl Pts',(1.70986873918469,0.676625335695913,5.88603596973901));
#18345=CARTESIAN_POINT('Ctrl Pts',(0.357828666998206,1.80372713991337,5.99723797068467));
#18346=CARTESIAN_POINT('Ctrl Pts',(-1.19324218206278,1.31842435999021,6.09991138930622));
#18347=CARTESIAN_POINT('Ctrl Pts',(-1.55187237400387,0.396890571994748,
6.16551747427924));
#18348=CARTESIAN_POINT('Ctrl Pts',(-1.55554339860443,-0.00142338748566248,
6.19405622560371));
#18349=CARTESIAN_POINT('Origin',(0.,0.,-1.2940562256037));
#18350=CARTESIAN_POINT('',(-1.55745457732731,-0.00085669689206486,4.6559437743963));
#18351=CARTESIAN_POINT('',(-1.55632403677708,0.00132295834575361,4.7940562256037));
#18352=CARTESIAN_POINT('',(-1.5555,-1.46451138874614E-13,-1.2940562256037));
#18353=CARTESIAN_POINT('Ctrl Pts',(-1.55745457732731,-0.000856696892064714,
4.6559437743963));
#18354=CARTESIAN_POINT('Ctrl Pts',(-1.55778497931963,-0.0507117794212508,
4.65952722214655));
#18355=CARTESIAN_POINT('Ctrl Pts',(-1.53299973239953,-0.615518763747496,
4.70014792479876));
#18356=CARTESIAN_POINT('Ctrl Pts',(-0.843969773291502,-1.63319857630279,
4.77780588235294));
#18357=CARTESIAN_POINT('Ctrl Pts',(0.914045851976043,-1.59503691128215,
4.88891764705882));
#18358=CARTESIAN_POINT('Ctrl Pts',(1.83578508816481,-0.0975483364234787,
5.0000294117647));
#18359=CARTESIAN_POINT('Ctrl Pts',(1.07793273566426,1.48918890180207,5.11114117647059));
#18360=CARTESIAN_POINT('Ctrl Pts',(-0.666138955726334,1.7134414082573,5.22225294117646));
#18361=CARTESIAN_POINT('Ctrl Pts',(-1.49940020022205,0.726840308291178,
5.30385380715171));
#18362=CARTESIAN_POINT('Ctrl Pts',(-1.55693103699923,0.106352731462292,
5.34841741822499));
#18363=CARTESIAN_POINT('Ctrl Pts',(-1.55596473934061,0.00138061827089576,
5.3559437743963));
#18364=CARTESIAN_POINT('Ctrl Pts',(-1.55632403677708,0.0013229583457536,
4.7940562256037));
#18365=CARTESIAN_POINT('Ctrl Pts',(-1.55249345266231,-0.422243736756442,
4.82444347081184));
#18366=CARTESIAN_POINT('Ctrl Pts',(-1.15449033772237,-1.36882487339263,
4.89189804966852));
#18367=CARTESIAN_POINT('Ctrl Pts',(0.447130949584586,-1.78368911643119,
4.99641996217376));
#18368=CARTESIAN_POINT('Ctrl Pts',(1.74141681985029,-0.590711782254083,
5.10762196311942));
#18369=CARTESIAN_POINT('Ctrl Pts',(1.44007996484097,1.14352203521175,5.21882396406507));
#18370=CARTESIAN_POINT('Ctrl Pts',(-0.18077114541208,1.82997124106871,5.33002596501073));
#18371=CARTESIAN_POINT('Ctrl Pts',(-1.38135491130028,1.01294047027372,5.42177005219028));
#18372=CARTESIAN_POINT('Ctrl Pts',(-1.55326847542029,0.247016435592901,
5.47644680572127));
#18373=CARTESIAN_POINT('Ctrl Pts',(-1.55296794440831,0.000212393646609865,
5.49405622560371));
#18374=CARTESIAN_POINT('Origin',(0.,0.,-1.2940562256037));
#18375=CARTESIAN_POINT('',(-1.55339110712961,-0.000825623642478797,3.9559437743963));
#18376=CARTESIAN_POINT('',(-1.55725058804626,-0.000987513992002087,4.0940562256037));
#18377=CARTESIAN_POINT('',(-1.5555,-1.46451138874614E-13,-1.2940562256037));
#18378=CARTESIAN_POINT('Ctrl Pts',(-1.55339110712961,-0.000825623642478918,
3.9559437743963));
#18379=CARTESIAN_POINT('Ctrl Pts',(-1.55438254706171,-0.206618413857449,
3.97063702606812));
#18380=CARTESIAN_POINT('Ctrl Pts',(-1.42060545887363,-0.929915671591215,
4.0223675326419));
#18381=CARTESIAN_POINT('Ctrl Pts',(-0.325144523748834,-1.80939315974833,
4.11113529411765));
#18382=CARTESIAN_POINT('Ctrl Pts',(1.34353857429153,-1.25480144535206,4.22224705882353));
#18383=CARTESIAN_POINT('Ctrl Pts',(1.7829949491126,0.447829855308947,4.33335882352941));
#18384=CARTESIAN_POINT('Ctrl Pts',(0.591158348240881,1.74073386109778,4.44447058823529));
#18385=CARTESIAN_POINT('Ctrl Pts',(-1.08565831565865,1.45067662979582,4.55199890519093));
#18386=CARTESIAN_POINT('Ctrl Pts',(-1.55437006059814,0.464572809188085,
4.62248996724459));
#18387=CARTESIAN_POINT('Ctrl Pts',(-1.55745457732731,-0.000856696892064714,
4.6559437743963));
#18388=CARTESIAN_POINT('Ctrl Pts',(-1.55725058804626,-0.000987513992001905,
4.0940562256037));
#18389=CARTESIAN_POINT('Ctrl Pts',(-1.55768831435815,-0.060125904161909,
4.09830546860531));
#18390=CARTESIAN_POINT('Ctrl Pts',(-1.52777409038815,-0.634697902152519,
4.13962204525546));
#18391=CARTESIAN_POINT('Ctrl Pts',(-0.813442378520323,-1.64917689984389,
4.21800595555418));
#18392=CARTESIAN_POINT('Ctrl Pts',(0.945308337362415,-1.57729676898942,
4.32920795649982));
#18393=CARTESIAN_POINT('Ctrl Pts',(1.83789338383513,-0.0601735806349488,
4.44040995744549));
#18394=CARTESIAN_POINT('Ctrl Pts',(1.04645630737228,1.51208536363268,4.55161195839114));
#18395=CARTESIAN_POINT('Ctrl Pts',(-0.703826144888774,1.69885305660096,
4.66281395933679));
#18396=CARTESIAN_POINT('Ctrl Pts',(-1.5071493991015,0.703327095585107,4.74362871507432));
#18397=CARTESIAN_POINT('Ctrl Pts',(-1.5571661216877,0.0944364658163476,
4.78737613716329));
#18398=CARTESIAN_POINT('Ctrl Pts',(-1.55632403677708,0.0013229583457536,
4.7940562256037));
#18399=CARTESIAN_POINT('Origin',(0.,0.,-1.2940562256037));
#18400=CARTESIAN_POINT('',(-1.55444728254952,0.00131753317857479,3.2559437743963));
#18401=CARTESIAN_POINT('',(-1.55328288481294,-0.000737459407344904,3.3940562256037));
#18402=CARTESIAN_POINT('',(-1.5555,-1.46451138874614E-13,-1.2940562256037));
#18403=CARTESIAN_POINT('Ctrl Pts',(-1.55444728254952,0.00131753317857487,
3.2559437743963));
#18404=CARTESIAN_POINT('Ctrl Pts',(-1.55154249309476,-0.359460968451768,
3.28174682998969));
#18405=CARTESIAN_POINT('Ctrl Pts',(-1.24689466125852,-1.24251939835746,
3.34458714048504));
#18406=CARTESIAN_POINT('Ctrl Pts',(0.2225644970039,-1.82485276462931,3.44446470588235));
#18407=CARTESIAN_POINT('Ctrl Pts',(1.65367987605646,-0.803097400934551,
3.55557647058823));
#18408=CARTESIAN_POINT('Ctrl Pts',(1.57181488059719,0.953425691385454,3.66668823529412));
#18409=CARTESIAN_POINT('Ctrl Pts',(0.05186921357973,1.83764309716413,3.7778));
#18410=CARTESIAN_POINT('Ctrl Pts',(-1.30826166492629,1.14597286376508,3.87421851303406));
#18411=CARTESIAN_POINT('Ctrl Pts',(-1.55188342608391,0.312123128070615,
3.93359977116616));
#18412=CARTESIAN_POINT('Ctrl Pts',(-1.55339110712961,-0.000825623642478918,
3.9559437743963));
#18413=CARTESIAN_POINT('Ctrl Pts',(-1.55328288481294,-0.000737459407344626,
3.3940562256037));
#18414=CARTESIAN_POINT('Ctrl Pts',(-1.55419278937645,-0.213364380143022,
3.40923480004733));
#18415=CARTESIAN_POINT('Ctrl Pts',(-1.41432753571211,-0.944097869976176,
3.4614807081395));
#18416=CARTESIAN_POINT('Ctrl Pts',(-0.300084107876245,-1.81422779119842,
3.55079394988024));
#18417=CARTESIAN_POINT('Ctrl Pts',(1.36219708122283,-1.23527003608861,3.66199595082589));
#18418=CARTESIAN_POINT('Ctrl Pts',(1.77632642388981,0.475539047756765,3.77319795177155));
#18419=CARTESIAN_POINT('Ctrl Pts',(0.562846122986205,1.75062194433623,3.8843999527172));
#18420=CARTESIAN_POINT('Ctrl Pts',(-1.10028173365827,1.43421840050251,3.99135271066126));
#18421=CARTESIAN_POINT('Ctrl Pts',(-1.55386990546895,0.455754792479586,
4.06123813495675));
#18422=CARTESIAN_POINT('Ctrl Pts',(-1.55725058804626,-0.000987513992001905,
4.0940562256037));
#18423=CARTESIAN_POINT('Origin',(0.,0.,-1.2940562256037));
#18424=CARTESIAN_POINT('',(-1.5580472770765,3.22739011431662E-5,2.5559437743963));
#18425=CARTESIAN_POINT('',(-1.55455103081039,0.00134678255213586,2.6940562256037));
#18426=CARTESIAN_POINT('',(-1.5555,-1.46451138874614E-13,-1.2940562256037));
#18427=CARTESIAN_POINT('Ctrl Pts',(-1.5580472770765,3.22739011430483E-5,
2.5559437743963));
#18428=CARTESIAN_POINT('Ctrl Pts',(-1.55789051448101,-0.513002401697162,
2.59285663391126));
#18429=CARTESIAN_POINT('Ctrl Pts',(-1.00059908603036,-1.54109252504942,
2.66680674832818));
#18430=CARTESIAN_POINT('Ctrl Pts',(0.750502303520728,-1.67820405842339,
2.77779411764705));
#18431=CARTESIAN_POINT('Ctrl Pts',(1.81691877690325,-0.280051291770722,
2.88890588235294));
#18432=CARTESIAN_POINT('Ctrl Pts',(1.221004776546,1.37432525375672,3.00001764705882));
#18433=CARTESIAN_POINT('Ctrl Pts',(-0.492027652059084,1.77130780998173,
3.11112941176471));
#18434=CARTESIAN_POINT('Ctrl Pts',(-1.4616245475244,0.831846153950699,3.1964381208772));
#18435=CARTESIAN_POINT('Ctrl Pts',(-1.55571197709572,0.158394185549965,
3.24470957508773));
#18436=CARTESIAN_POINT('Ctrl Pts',(-1.55444728254952,0.00131753317857487,
3.2559437743963));
#18437=CARTESIAN_POINT('Ctrl Pts',(-1.55455103081039,0.00134678255213593,
2.6940562256037));
#18438=CARTESIAN_POINT('Ctrl Pts',(-1.55153631123715,-0.363632076962094,
2.72016413148935));
#18439=CARTESIAN_POINT('Ctrl Pts',(-1.2410339082364,-1.25141700119195,2.78333937102354));
#18440=CARTESIAN_POINT('Ctrl Pts',(0.239078896742882,-1.82327020255007,
2.88358194420631));
#18441=CARTESIAN_POINT('Ctrl Pts',(1.66194822130476,-0.787020368122459,
2.99478394515195));
#18442=CARTESIAN_POINT('Ctrl Pts',(1.56201018579718,0.970359278599158,3.10598594609762));
#18443=CARTESIAN_POINT('Ctrl Pts',(0.0308358597469676,1.83861961806662,
3.21718794704326));
#18444=CARTESIAN_POINT('Ctrl Pts',(-1.31573769524687,1.1336310555357,3.3132113735453));
#18445=CARTESIAN_POINT('Ctrl Pts',(-1.55197072720788,0.305888138784002,
3.37216746639878));
#18446=CARTESIAN_POINT('Ctrl Pts',(-1.55328288481294,-0.000737459407344626,
3.3940562256037));
#18447=CARTESIAN_POINT('Origin',(0.,0.,-1.2940562256037));
#18448=CARTESIAN_POINT('',(-1.55454106205097,-0.00133830406313126,1.8559437743963));
#18449=CARTESIAN_POINT('',(-1.55805738347505,7.8333006204296E-6,1.9940562256037));
#18450=CARTESIAN_POINT('',(-1.5555,-1.46451138874614E-13,-1.2940562256037));
#18451=CARTESIAN_POINT('Ctrl Pts',(-1.55454106205097,-0.00133830406313111,
1.8559437743963));
#18452=CARTESIAN_POINT('Ctrl Pts',(-1.55580278448011,-0.154912931015377,
1.86692918293086));
#18453=CARTESIAN_POINT('Ctrl Pts',(-1.4643553294945,-0.824794260236109,
1.91495184636739));
#18454=CARTESIAN_POINT('Ctrl Pts',(-0.503883253349445,-1.76797174153445,
2.00001176470588));
#18455=CARTESIAN_POINT('Ctrl Pts',(1.21177025569706,-1.38247440008765,2.11112352941176));
#18456=CARTESIAN_POINT('Ctrl Pts',(1.81875417317235,0.267872803846544,2.22223529411764));
#18457=CARTESIAN_POINT('Ctrl Pts',(0.761728374059259,1.67313849696631,2.33334705882353));
#18458=CARTESIAN_POINT('Ctrl Pts',(-0.992215910389441,1.54762080750275,
2.44445882352941));
#18459=CARTESIAN_POINT('Ctrl Pts',(-1.5572623887173,0.518253196217567,2.51865772872033));
#18460=CARTESIAN_POINT('Ctrl Pts',(-1.55804780536241,0.00176118756036677,
2.5558193790093));
#18461=CARTESIAN_POINT('Ctrl Pts',(-1.5580472770765,3.22739011430483E-5,
2.5559437743963));
#18462=CARTESIAN_POINT('Ctrl Pts',(-1.55805738347505,7.83330062046083E-6,
1.9940562256037));
#18463=CARTESIAN_POINT('Ctrl Pts',(-1.55801899566519,-0.514746844163175,
2.03109346293137));
#18464=CARTESIAN_POINT('Ctrl Pts',(-0.997193073467916,-1.54474611801162,
2.1051980339076));
#18465=CARTESIAN_POINT('Ctrl Pts',(0.757683106401647,-1.67552656471375,
2.21636993853236));
#18466=CARTESIAN_POINT('Ctrl Pts',(1.81878565659978,-0.271093501731151,
2.32757193947802));
#18467=CARTESIAN_POINT('Ctrl Pts',(1.2133740808,1.38173669240563,2.43877394042368));
#18468=CARTESIAN_POINT('Ctrl Pts',(-0.50382603046139,1.76851131819754,2.54997594136933));
#18469=CARTESIAN_POINT('Ctrl Pts',(-1.46460308673025,0.824478033792379,
2.63507003642934));
#18470=CARTESIAN_POINT('Ctrl Pts',(-1.55581653259107,0.154555525656757,
2.6830967978408));
#18471=CARTESIAN_POINT('Ctrl Pts',(-1.55455103081039,0.00134678255213593,
2.6940562256037));
#18472=CARTESIAN_POINT('Origin',(0.,0.,-1.2940562256037));
#18473=CARTESIAN_POINT('',(-1.55333654104773,0.00077999677327307,1.1559437743963));
#18474=CARTESIAN_POINT('',(-1.55457410202289,-0.00135137241159503,1.2940562256037));
#18475=CARTESIAN_POINT('',(-1.5555,-1.46451138874614E-13,-1.2940562256037));
#18476=CARTESIAN_POINT('Ctrl Pts',(-1.55333654104773,0.000779996773273093,
1.1559437743963));
#18477=CARTESIAN_POINT('Ctrl Pts',(-1.55193441184992,-0.308712050983944,
1.17803898685243));
#18478=CARTESIAN_POINT('Ctrl Pts',(-1.31241259724573,-1.13899385066835,
1.23717145421053));
#18479=CARTESIAN_POINT('Ctrl Pts',(0.0395573460867233,-1.83794734661457,
1.33334117647059));
#18480=CARTESIAN_POINT('Ctrl Pts',(1.56539206925502,-0.963935520329204,
1.44445294117647));
#18481=CARTESIAN_POINT('Ctrl Pts',(1.65902311109036,0.792001314055404,1.55556470588235));
#18482=CARTESIAN_POINT('Ctrl Pts',(0.234784819358076,1.82332048051019,1.66667647058823));
#18483=CARTESIAN_POINT('Ctrl Pts',(-1.24221255679906,1.24941902193381,1.76680282675955));
#18484=CARTESIAN_POINT('Ctrl Pts',(-1.55154889304983,0.362863225147233,
1.8298919280289));
#18485=CARTESIAN_POINT('Ctrl Pts',(-1.55454106205097,-0.00133830406313111,
1.8559437743963));
#18486=CARTESIAN_POINT('Ctrl Pts',(-1.55457410202289,-0.00135137241159506,
1.2940562256037));
#18487=CARTESIAN_POINT('Ctrl Pts',(-1.55583838883925,-0.153712992066033,
1.30495546072484));
#18488=CARTESIAN_POINT('Ctrl Pts',(-1.46525911062305,-0.822772247294108,
1.35292202949453));
#18489=CARTESIAN_POINT('Ctrl Pts',(-0.506691785521986,-1.76769208329225,
1.43795593191277));
#18490=CARTESIAN_POINT('Ctrl Pts',(1.21113283005724,-1.38370173748454,1.54915793285843));
#18491=CARTESIAN_POINT('Ctrl Pts',(1.81922269924897,0.268145221691032,1.66035993380409));
#18492=CARTESIAN_POINT('Ctrl Pts',(0.760397896971566,1.67429621989364,1.77156193474974));
#18493=CARTESIAN_POINT('Ctrl Pts',(-0.99516307107971,1.54632579451077,1.8827639356954));
#18494=CARTESIAN_POINT('Ctrl Pts',(-1.55786775595712,0.516017344817124,
1.95692869931338));
#18495=CARTESIAN_POINT('Ctrl Pts',(-1.55805741466885,0.000426121031216267,
1.99402612928282));
#18496=CARTESIAN_POINT('Ctrl Pts',(-1.55805738347505,7.83330062046083E-6,
1.9940562256037));
#18497=CARTESIAN_POINT('Origin',(0.,0.,-1.2940562256037));
#18498=CARTESIAN_POINT('',(-1.55735939632673,0.00101326450419681,0.455943774396298));
#18499=CARTESIAN_POINT('',(-1.55326674879324,0.000737490386717859,0.594056225603704));
#18500=CARTESIAN_POINT('',(-1.5555,-1.46451138874614E-13,-1.2940562256037));
#18501=CARTESIAN_POINT('Ctrl Pts',(-1.55735939632673,0.00101326450419686,
0.455943774396298));
#18502=CARTESIAN_POINT('Ctrl Pts',(-1.55415403990615,-0.460986485095401,
0.489148790774002));
#18503=CARTESIAN_POINT('Ctrl Pts',(-1.09150770385912,-1.44424025370235,
0.559391062053666));
#18504=CARTESIAN_POINT('Ctrl Pts',(0.579500018064921,-1.74455968620895,
0.666670588235291));
#18505=CARTESIAN_POINT('Ctrl Pts',(1.77994595636936,-0.459814902815864,
0.777782352941175));
#18506=CARTESIAN_POINT('Ctrl Pts',(1.35191942796293,1.24579875779621,0.888894117647056));
#18507=CARTESIAN_POINT('Ctrl Pts',(-0.31301785631821,1.81151698861828,1.00000588235294));
#18508=CARTESIAN_POINT('Ctrl Pts',(-1.41742989907648,0.936970735614399,
1.08902243460269));
#18509=CARTESIAN_POINT('Ctrl Pts',(-1.55428474075524,0.210076165498259,
1.14100173195047));
#18510=CARTESIAN_POINT('Ctrl Pts',(-1.55333654104773,0.000779996773273093,
1.1559437743963));
#18511=CARTESIAN_POINT('Ctrl Pts',(-1.55326674879324,0.000737490386717929,
0.594056225603704));
#18512=CARTESIAN_POINT('Ctrl Pts',(-1.55198188529325,-0.305056076963429,
0.615884792166863));
#18513=CARTESIAN_POINT('Ctrl Pts',(-1.31673706663562,-1.13196023879971,
0.674780692378575));
#18514=CARTESIAN_POINT('Ctrl Pts',(0.0278603330084876,-1.83865390028585,
0.770743926238836));
#18515=CARTESIAN_POINT('Ctrl Pts',(1.5604328654528,-0.972896783194139,0.881945927184494));
#18516=CARTESIAN_POINT('Ctrl Pts',(1.66322297628929,0.784329206349798,0.993147928130148));
#18517=CARTESIAN_POINT('Ctrl Pts',(0.242033178606095,1.82287837028977,1.10434992907581));
#18518=CARTESIAN_POINT('Ctrl Pts',(-1.23989296747105,1.25308568603502,1.20465269490032));
#18519=CARTESIAN_POINT('Ctrl Pts',(-1.55153866131449,0.364455386558259,
1.26788812707629));
#18520=CARTESIAN_POINT('Ctrl Pts',(-1.55457410202289,-0.00135137241159506,
1.2940562256037));
#18521=CARTESIAN_POINT('Origin',(0.,0.,9.5));
#18522=CARTESIAN_POINT('',(-1.8436644593731,-0.000635433610831735,9.15893008989225));
#18523=CARTESIAN_POINT('Ctrl Pts',(0.964986447796868,1.2199923793075,9.4445));
#18524=CARTESIAN_POINT('Ctrl Pts',(1.01353513125755,1.18505085067097,9.44178677406621));
#18525=CARTESIAN_POINT('Ctrl Pts',(1.0597539884705,1.14720650264821,9.43908619037108));
#18526=CARTESIAN_POINT('Ctrl Pts',(1.10357643916964,1.10678728284429,9.43639370111374));
#18527=CARTESIAN_POINT('Ctrl Pts',(1.14671113352339,1.0670024085517,9.43374346820086));
#18528=CARTESIAN_POINT('Ctrl Pts',(1.18752436163327,1.02472203468752,9.43110107764874));
#18529=CARTESIAN_POINT('Ctrl Pts',(1.22592701109647,0.980220056324443,9.4284621924353));
#18530=CARTESIAN_POINT('Ctrl Pts',(1.24656064684413,0.956309268281708,9.42704432681834));
#18531=CARTESIAN_POINT('Ctrl Pts',(1.2664979086022,0.931756532766836,9.42562747315155));
#18532=CARTESIAN_POINT('Ctrl Pts',(1.28572135928109,0.906600809401326,9.42421095871337));
#18533=CARTESIAN_POINT('Ctrl Pts',(1.29315226707552,0.896876756006653,9.42366339894611));
#18534=CARTESIAN_POINT('Ctrl Pts',(1.30047431632806,0.887065294343418,9.42311604538434));
#18535=CARTESIAN_POINT('Ctrl Pts',(1.30768090461229,0.877176902486747,9.4225693022564));
#18536=CARTESIAN_POINT('Ctrl Pts',(1.34465595997822,0.826442238321084,9.4197641111411));
#18537=CARTESIAN_POINT('Ctrl Pts',(1.37864083403329,0.773625333680106,9.41697158537819));
#18538=CARTESIAN_POINT('Ctrl Pts',(1.40953528457578,0.719059333620718,9.41418667925324));
#18539=CARTESIAN_POINT('Ctrl Pts',(1.44068034022624,0.664050713022807,9.41137918293207));
#18540=CARTESIAN_POINT('Ctrl Pts',(1.46868519868955,0.607263591678243,9.40857943036595));
#18541=CARTESIAN_POINT('Ctrl Pts',(1.4934057683288,0.549006709906255,9.40578225205449));
#18542=CARTESIAN_POINT('Ctrl Pts',(1.49984356600261,0.533835295030795,9.40505380330555));
#18543=CARTESIAN_POINT('Ctrl Pts',(1.50605838114916,0.518564071644944,9.40432552914253));
#18544=CARTESIAN_POINT('Ctrl Pts',(1.51204713790707,0.503198254185902,9.40359733826241));
#18545=CARTESIAN_POINT('Ctrl Pts',(1.51578438435043,0.493609311276813,9.40314291526832));
#18546=CARTESIAN_POINT('Ctrl Pts',(1.51943283421544,0.483985318888239,9.40268861051374));
#18547=CARTESIAN_POINT('Ctrl Pts',(1.52298881285553,0.474336147548569,9.40223480218929));
#18548=CARTESIAN_POINT('Ctrl Pts',(1.54512657800669,0.414265176757972,9.39940961589683));
#18549=CARTESIAN_POINT('Ctrl Pts',(1.56372018959743,0.353128682437969,9.39659929425661));
#18550=CARTESIAN_POINT('Ctrl Pts',(1.57865714116174,0.291257786036896,9.39379872614803));
#18551=CARTESIAN_POINT('Ctrl Pts',(1.59350224792573,0.229767323360879,9.39101537826123));
#18552=CARTESIAN_POINT('Ctrl Pts',(1.60473597791275,0.167550465196752,9.38824166432918));
#18553=CARTESIAN_POINT('Ctrl Pts',(1.612201835455,0.104910300904696,9.38547256693499));
#18554=CARTESIAN_POINT('Ctrl Pts',(1.61736371100559,0.0616010453082987,
9.38355801980422));
#18555=CARTESIAN_POINT('Ctrl Pts',(1.62072348102385,0.0180889750237585,
9.38164567951963));
#18556=CARTESIAN_POINT('Ctrl Pts',(1.62221464959515,-0.0255281734684064,
9.379733887779));
#18557=CARTESIAN_POINT('Ctrl Pts',(1.62311301667558,-0.0518056923901331,
9.37858211272319));
#18558=CARTESIAN_POINT('Ctrl Pts',(1.6233329220732,-0.0781213723415495,
9.37743053676479));
#18559=CARTESIAN_POINT('Ctrl Pts',(1.6228574829942,-0.104453779990354,9.37627879728949));
#18560=CARTESIAN_POINT('Ctrl Pts',(1.62265929679902,-0.115430411724188,
9.3757986961061));
#18561=CARTESIAN_POINT('Ctrl Pts',(1.6223401558167,-0.126409918390069,9.37531856781002));
#18562=CARTESIAN_POINT('Ctrl Pts',(1.62189965557521,-0.137376114393304,
9.37483902548745));
#18563=CARTESIAN_POINT('Ctrl Pts',(1.6216428503266,-0.143769247530682,9.37455945927212));
#18564=CARTESIAN_POINT('Ctrl Pts',(1.62134478429418,-0.15015909919995,9.37428003787639));
#18565=CARTESIAN_POINT('Ctrl Pts',(1.62100533439947,-0.156545355045619,
9.37400075635211));
#18566=CARTESIAN_POINT('Ctrl Pts',(1.61776588850122,-0.217490816000868,
9.37133551060487));
#18567=CARTESIAN_POINT('Ctrl Pts',(1.61076184583078,-0.27810811078512,9.36868300338423));
#18568=CARTESIAN_POINT('Ctrl Pts',(1.60024388638002,-0.33815222699736,9.36603893410604));
#18569=CARTESIAN_POINT('Ctrl Pts',(1.58926239194622,-0.400842535992609,
9.36327833855545));
#18570=CARTESIAN_POINT('Ctrl Pts',(1.5744503497123,-0.462908874929355,9.3605269410697));
#18571=CARTESIAN_POINT('Ctrl Pts',(1.55603619221491,-0.524074243638481,
9.35777984704762));
#18572=CARTESIAN_POINT('Ctrl Pts',(1.54065020182884,-0.575181103947007,
9.35548450650763));
#18573=CARTESIAN_POINT('Ctrl Pts',(1.52274824032724,-0.625659260102185,
9.35319217042017));
#18574=CARTESIAN_POINT('Ctrl Pts',(1.50243626590723,-0.675341229990148,
9.35089998357483));
#18575=CARTESIAN_POINT('Ctrl Pts',(1.49675934867098,-0.689226656653057,
9.35025934890575));
#18576=CARTESIAN_POINT('Ctrl Pts',(1.49089404119114,-0.70304983797203,9.34961872589435));
#18577=CARTESIAN_POINT('Ctrl Pts',(1.48484234501078,-0.716806975404219,
9.34897805220743));
#18578=CARTESIAN_POINT('Ctrl Pts',(1.47962711111297,-0.728662608492026,
9.34842593210261));
#18579=CARTESIAN_POINT('Ctrl Pts',(1.47427261241135,-0.74047069735123,9.34787370156138));
#18580=CARTESIAN_POINT('Ctrl Pts',(1.46878946750842,-0.752209477846282,
9.34732223297784));
#18581=CARTESIAN_POINT('Ctrl Pts',(1.44124114383179,-0.811187259825758,
9.34455155386835));
#18582=CARTESIAN_POINT('Ctrl Pts',(1.41040240116235,-0.868527008616387,
9.34179496514958));
#18583=CARTESIAN_POINT('Ctrl Pts',(1.3765156583388,-0.923951665257498,9.33904765215105));
#18584=CARTESIAN_POINT('Ctrl Pts',(1.34221268254424,-0.98005710640542,9.33626659373598));
#18585=CARTESIAN_POINT('Ctrl Pts',(1.30478591472408,-1.03420112061383,9.3334950403091));
#18586=CARTESIAN_POINT('Ctrl Pts',(1.26443637894511,-1.08608026731007,9.33072799759508));
#18587=CARTESIAN_POINT('Ctrl Pts',(1.23112993903158,-1.1289038004399,9.32844394797434));
#18588=CARTESIAN_POINT('Ctrl Pts',(1.19583096929852,-1.17018410899034,9.32616297179209));
#18589=CARTESIAN_POINT('Ctrl Pts',(1.15863053726262,-1.20973500520381,9.32388226011456));
#18590=CARTESIAN_POINT('Ctrl Pts',(1.14503499841471,-1.22418956168373,9.32304873473553));
#18591=CARTESIAN_POINT('Ctrl Pts',(1.13118531407677,-1.23841295906892,9.32221524468542));
#18592=CARTESIAN_POINT('Ctrl Pts',(1.11708535825451,-1.25239547008276,9.32138165284865));
#18593=CARTESIAN_POINT('Ctrl Pts',(1.10886443632285,-1.26054791629624,9.32089563051642));
#18594=CARTESIAN_POINT('Ctrl Pts',(1.10055776106962,-1.26861897429176,9.3204095386295));
#18595=CARTESIAN_POINT('Ctrl Pts',(1.09217814991772,-1.27659553689908,9.31992403906899));
#18596=CARTESIAN_POINT('Ctrl Pts',(1.0442665456713,-1.32220265445632,9.31714812711039));
#18597=CARTESIAN_POINT('Ctrl Pts',(0.993885467018336,-1.36481211874555,
9.31438629338051));
#18598=CARTESIAN_POINT('Ctrl Pts',(0.941242813634035,-1.40412918747402,
9.31163369987499));
#18599=CARTESIAN_POINT('Ctrl Pts',(0.889258180215484,-1.4429548027032,9.30891551309799));
#18600=CARTESIAN_POINT('Ctrl Pts',(0.835067536107577,-1.47857067848576,
9.30620633698811));
#18601=CARTESIAN_POINT('Ctrl Pts',(0.778833889995821,-1.51065975001959,
9.30350151270422));
#18602=CARTESIAN_POINT('Ctrl Pts',(0.722586441970542,-1.54275669745372,
9.30079602455175));
#18603=CARTESIAN_POINT('Ctrl Pts',(0.664294246016674,-1.57132562044258,
9.29809489036176));
#18604=CARTESIAN_POINT('Ctrl Pts',(0.60428947258743,-1.59639249571732,9.2953934478619));
#18605=CARTESIAN_POINT('Ctrl Pts',(0.591343331742152,-1.60180072041865,
9.29481060664627));
#18606=CARTESIAN_POINT('Ctrl Pts',(0.57831739582737,-1.60704575229747,9.29422775107918));
#18607=CARTESIAN_POINT('Ctrl Pts',(0.565214891376733,-1.61212755946014,
9.2936448343374));
#18608=CARTESIAN_POINT('Ctrl Pts',(0.555972206658096,-1.6157123353007,9.29323363694519));
#18609=CARTESIAN_POINT('Ctrl Pts',(0.546693262642617,-1.61921511430512,
9.29282249204174));
#18610=CARTESIAN_POINT('Ctrl Pts',(0.537387803700891,-1.62263297583653,
9.29241175882646));
#18611=CARTESIAN_POINT('Ctrl Pts',(0.475984234705077,-1.64518628542356,
9.28970146957778));
#18612=CARTESIAN_POINT('Ctrl Pts',(0.413324985792773,-1.66408644383074,
9.2870044827103));
#18613=CARTESIAN_POINT('Ctrl Pts',(0.349771964499173,-1.67941338858561,
9.28431629702065));
#18614=CARTESIAN_POINT('Ctrl Pts',(0.284907818691178,-1.69505653440519,
9.2815726529738));
#18615=CARTESIAN_POINT('Ctrl Pts',(0.219111690562125,-1.70697771722454,
9.2788381769944));
#18616=CARTESIAN_POINT('Ctrl Pts',(0.152743105316565,-1.71521251897908,
9.27610808350735));
#18617=CARTESIAN_POINT('Ctrl Pts',(0.108619750041913,-1.72068720375785,
9.27429305483955));
#18618=CARTESIAN_POINT('Ctrl Pts',(0.0642428719693675,-1.72453152305287,
9.27247996318729));
#18619=CARTESIAN_POINT('Ctrl Pts',(0.0197153791249731,-1.72674355800955,
9.27066740233454));
#18620=CARTESIAN_POINT('Ctrl Pts',(-0.00935520099652008,-1.72818772509222,
9.26948403915532));
#18621=CARTESIAN_POINT('Ctrl Pts',(-0.0384900123738061,-1.72893595074551,
9.26830090222237));
#18622=CARTESIAN_POINT('Ctrl Pts',(-0.0676604159497131,-1.72898539458108,
9.26711760021896));
#18623=CARTESIAN_POINT('Ctrl Pts',(-0.0792958143034031,-1.72900511658189,
9.26664560845695));
#18624=CARTESIAN_POINT('Ctrl Pts',(-0.0909391905971971,-1.72891359625761,
9.26617349650779));
#18625=CARTESIAN_POINT('Ctrl Pts',(-0.102581232900295,-1.72871071219562,
9.26570154289531));
#18626=CARTESIAN_POINT('Ctrl Pts',(-0.170900558303332,-1.72752012192893,
9.26293196419191));
#18627=CARTESIAN_POINT('Ctrl Pts',(-0.238956647295054,-1.72250403767711,
9.26017659214973));
#18628=CARTESIAN_POINT('Ctrl Pts',(-0.30637923630299,-1.71371181735864,
9.25743063944084));
#18629=CARTESIAN_POINT('Ctrl Pts',(-0.373589954383447,-1.70494722599808,
9.25469331570268));
#18630=CARTESIAN_POINT('Ctrl Pts',(-0.440172255573728,-1.69243020084097,
9.25196535219159));
#18631=CARTESIAN_POINT('Ctrl Pts',(-0.505764774523597,-1.67615838081314,
9.24924200656954));
#18632=CARTESIAN_POINT('Ctrl Pts',(-0.571106403622123,-1.65994880011646,
9.24652907768082));
#18633=CARTESIAN_POINT('Ctrl Pts',(-0.635466898101783,-1.64001312037568,
9.24382073142206));
#18634=CARTESIAN_POINT('Ctrl Pts',(-0.698478020047089,-1.6162978205588,
9.24111227966534));
#18635=CARTESIAN_POINT('Ctrl Pts',(-0.714257342673809,-1.61035900602182,
9.24043402584651));
#18636=CARTESIAN_POINT('Ctrl Pts',(-0.729951945569458,-1.60418291559246,
9.23975576541181));
#18637=CARTESIAN_POINT('Ctrl Pts',(-0.745555812125029,-1.59776819932882,
9.23907742473836));
#18638=CARTESIAN_POINT('Ctrl Pts',(-0.758165841483652,-1.59258424315208,
9.23852923395649));
#18639=CARTESIAN_POINT('Ctrl Pts',(-0.7707186000527,-1.58724342153027,9.23798090121265));
#18640=CARTESIAN_POINT('Ctrl Pts',(-0.783190247921723,-1.58175442379625,
9.23743329902252));
#18641=CARTESIAN_POINT('Ctrl Pts',(-0.816912656931304,-1.56691258183734,
9.23595262339534));
#18642=CARTESIAN_POINT('Ctrl Pts',(-0.850075178494816,-1.55097461965651,
9.23447585783886));
#18643=CARTESIAN_POINT('Ctrl Pts',(-0.882621385021603,-1.53394288417305,
9.23300226905634));
#18644=CARTESIAN_POINT('Ctrl Pts',(-0.940729021590098,-1.50353461232764,
9.23037133996924));
#18645=CARTESIAN_POINT('Ctrl Pts',(-0.996873413800297,-1.46964284065132,
9.22775053721005));
#18646=CARTESIAN_POINT('Ctrl Pts',(-1.05092798108356,-1.43259472728442,
9.22513568749178));
#18647=CARTESIAN_POINT('Ctrl Pts',(-1.10572540080839,-1.39503747504446,
9.22248490283599));
#18648=CARTESIAN_POINT('Ctrl Pts',(-1.15837574574728,-1.35423590514407,
9.21984023596641));
#18649=CARTESIAN_POINT('Ctrl Pts',(-1.20872367105371,-1.3104847487346,9.21719733916479));
#18650=CARTESIAN_POINT('Ctrl Pts',(-1.23098837194441,-1.29113725020014,
9.21602860566852));
#18651=CARTESIAN_POINT('Ctrl Pts',(-1.25280246308233,-1.27121240133872,
9.21486021831921));
#18652=CARTESIAN_POINT('Ctrl Pts',(-1.27415061053865,-1.25073337083793,
9.21369180113468));
#18653=CARTESIAN_POINT('Ctrl Pts',(-1.28784402235457,-1.23759743954403,
9.21294233949107));
#18654=CARTESIAN_POINT('Ctrl Pts',(-1.301345702892,-1.224233470889,9.21219286557216));
#18655=CARTESIAN_POINT('Ctrl Pts',(-1.31465131341234,-1.2106473229253,9.21144328015282));
#18656=CARTESIAN_POINT('Ctrl Pts',(-1.32306845489082,-1.20205271320159,
9.21096909172567));
#18657=CARTESIAN_POINT('Ctrl Pts',(-1.33140768074567,-1.19336846646048,
9.21049482332023));
#18658=CARTESIAN_POINT('Ctrl Pts',(-1.33965658703659,-1.1846083807011,9.21002110694334));
#18659=CARTESIAN_POINT('Ctrl Pts',(-1.38683756934781,-1.13450362296938,
9.20731160786425));
#18660=CARTESIAN_POINT('Ctrl Pts',(-1.43115584257498,-1.08183136746067,
9.20461514627079));
#18661=CARTESIAN_POINT('Ctrl Pts',(-1.47246637362013,-1.0269335551328,9.20192723192248));
#18662=CARTESIAN_POINT('Ctrl Pts',(-1.51435673419381,-0.971265203868867,
9.19920159033926));
#18663=CARTESIAN_POINT('Ctrl Pts',(-1.55315502041598,-0.91330760001291,
9.1964847376212));
#18664=CARTESIAN_POINT('Ctrl Pts',(-1.58867598518827,-0.853376054373785,
9.19377199178822));
#18665=CARTESIAN_POINT('Ctrl Pts',(-1.6230423285283,-0.795392604669187,
9.19114742471105));
#18666=CARTESIAN_POINT('Ctrl Pts',(-1.65434131270559,-0.735560522670982,
9.18852670186681));
#18667=CARTESIAN_POINT('Ctrl Pts',(-1.68236622824247,-0.674140102529266,
9.1859055831635));
#18668=CARTESIAN_POINT('Ctrl Pts',(-1.69115054831466,-0.654888068431862,
9.18508400189569));
#18669=CARTESIAN_POINT('Ctrl Pts',(-1.69961287778241,-0.63547984453725,
9.18426238173516));
#18670=CARTESIAN_POINT('Ctrl Pts',(-1.70774593841608,-0.615923128385269,
9.18344059210489));
#18671=CARTESIAN_POINT('Ctrl Pts',(-1.71216302078559,-0.605301834629889,
9.18299427642487));
#18672=CARTESIAN_POINT('Ctrl Pts',(-1.71647899938211,-0.594646287471263,
9.18254831195315));
#18673=CARTESIAN_POINT('Ctrl Pts',(-1.72069300111537,-0.583958415385776,
9.18210269794168));
#18674=CARTESIAN_POINT('Ctrl Pts',(-1.7465485778942,-0.518381532697819,
9.17936857298954));
#18675=CARTESIAN_POINT('Ctrl Pts',(-1.76857092720554,-0.451584515773078,
9.17664740083961));
#18676=CARTESIAN_POINT('Ctrl Pts',(-1.78657879748973,-0.383887803013472,
9.17393456255171));
#18677=CARTESIAN_POINT('Ctrl Pts',(-1.804265940182,-0.317396796610095,9.17127004103185));
#18678=CARTESIAN_POINT('Ctrl Pts',(-1.818080791813,-0.250036934098204,9.16861355915858));
#18679=CARTESIAN_POINT('Ctrl Pts',(-1.82780692425633,-0.182090439888411,
9.16596074041796));
#18680=CARTESIAN_POINT('Ctrl Pts',(-1.83203474093648,-0.152555028639186,
9.16480759641274));
#18681=CARTESIAN_POINT('Ctrl Pts',(-1.83548936700523,-0.122908576611995,
9.16365514456446));
#18682=CARTESIAN_POINT('Ctrl Pts',(-1.83814997966601,-0.0931736312707507,
9.16250302540846));
#18683=CARTESIAN_POINT('Ctrl Pts',(-1.84090084649807,-0.0624300074061506,
9.16131182369032));
#18684=CARTESIAN_POINT('Ctrl Pts',(-1.8428029176425,-0.0315917693259644,
9.16012097761867));
#18685=CARTESIAN_POINT('Ctrl Pts',(-1.84387051712372,-0.000685899417074366,
9.15893008989225));
#18686=CARTESIAN_POINT('',(1.57682165668711,1.14877748587887,9.046));
#18687=CARTESIAN_POINT('Ctrl Pts',(1.57638112755701,1.14851130170693,9.046));
#18688=CARTESIAN_POINT('Ctrl Pts',(1.52665365100122,1.20039535614393,9.05556311183685));
#18689=CARTESIAN_POINT('Ctrl Pts',(1.47436073626302,1.24949348117112,9.06516696825537));
#18690=CARTESIAN_POINT('Ctrl Pts',(1.41972944071722,1.2955534749412,9.07483034464178));
#18691=CARTESIAN_POINT('Ctrl Pts',(1.3664938249483,1.3404367621883,9.08424684826298));
#18692=CARTESIAN_POINT('Ctrl Pts',(1.31103689266819,1.38243551265733,9.09371986955463));
#18693=CARTESIAN_POINT('Ctrl Pts',(1.25355103002689,1.42127113207222,9.10326678137301));
#18694=CARTESIAN_POINT('Ctrl Pts',(1.21505546529212,1.44727751055399,9.10965989691543));
#18695=CARTESIAN_POINT('Ctrl Pts',(1.17564971559358,1.4718644964471,9.11608614753966));
#18696=CARTESIAN_POINT('Ctrl Pts',(1.1353897956679,1.4949355025024,9.12255075023748));
#18697=CARTESIAN_POINT('Ctrl Pts',(1.10085612021387,1.5147250757798,9.12809588028041));
#18698=CARTESIAN_POINT('Ctrl Pts',(1.06569392033189,1.53339909402576,9.13366922848017));
#18699=CARTESIAN_POINT('Ctrl Pts',(1.02993870461658,1.55088989389757,9.13927408736756));
#18700=CARTESIAN_POINT('Ctrl Pts',(1.01974786900349,1.55587506494657,9.14087156606859));
#18701=CARTESIAN_POINT('Ctrl Pts',(1.00951092351917,1.56076299370641,9.14247127864936));
#18702=CARTESIAN_POINT('Ctrl Pts',(0.99923854738173,1.56554780312885,9.14407178199195));
#18703=CARTESIAN_POINT('Ctrl Pts',(0.938937254424059,1.59363577331886,9.15346711756474));
#18704=CARTESIAN_POINT('Ctrl Pts',(0.877320674058788,1.61822126093367,9.16290462306444));
#18705=CARTESIAN_POINT('Ctrl Pts',(0.814565971029498,1.6390607692062,9.17240255066083));
#18706=CARTESIAN_POINT('Ctrl Pts',(0.794337488449258,1.64577822000625,9.1754641325608));
#18707=CARTESIAN_POINT('Ctrl Pts',(0.773990691920164,1.65210605100162,9.17853199258413));
#18708=CARTESIAN_POINT('Ctrl Pts',(0.753531412608169,1.65803494195743,9.18160674204658));
#18709=CARTESIAN_POINT('Ctrl Pts',(0.685680963865546,1.67769731157287,9.19180373518681));
#18710=CARTESIAN_POINT('Ctrl Pts',(0.616592242438488,1.69297649589436,9.20207650030987));
#18711=CARTESIAN_POINT('Ctrl Pts',(0.546660605554544,1.70392247702929,9.21244733474057));
#18712=CARTESIAN_POINT('Ctrl Pts',(0.485470423281094,1.71350021052235,9.22152181486743));
#18713=CARTESIAN_POINT('Ctrl Pts',(0.423634394293533,1.7197591669622,9.23067137930796));
#18714=CARTESIAN_POINT('Ctrl Pts',(0.361433447993987,1.72269786116138,9.23991096552778));
#18715=CARTESIAN_POINT('Ctrl Pts',(0.349628912262679,1.72325556844304,9.24166446016352));
#18716=CARTESIAN_POINT('Ctrl Pts',(0.337810284535043,1.72369353857676,9.24342134888598));
#18717=CARTESIAN_POINT('Ctrl Pts',(0.325996288505707,1.72401147004967,9.24517924372526));
#18718=CARTESIAN_POINT('Ctrl Pts',(0.260416164444351,1.72577632466661,9.25493741203347));
#18719=CARTESIAN_POINT('Ctrl Pts',(0.194857285865191,1.72385320378291,9.26474446521909));
#18720=CARTESIAN_POINT('Ctrl Pts',(0.129635755801097,1.71831420943767,9.27462138494297));
#18721=CARTESIAN_POINT('Ctrl Pts',(0.0648376826768893,1.71281117753602,
9.28443417783331));
#18722=CARTESIAN_POINT('Ctrl Pts',(0.00037157230131897,1.70373855506801,
9.29431593297685));
#18723=CARTESIAN_POINT('Ctrl Pts',(-0.0634310656618756,1.69112091958725,
9.3042872260058));
#18724=CARTESIAN_POINT('Ctrl Pts',(-0.125882183323273,1.67877056130784,
9.31404729885022));
#18725=CARTESIAN_POINT('Ctrl Pts',(-0.187698423459061,1.66302322279157,
9.32389315642556));
#18726=CARTESIAN_POINT('Ctrl Pts',(-0.248535080977911,1.64386571170743,
9.33384409431584));
#18727=CARTESIAN_POINT('Ctrl Pts',(-0.264799294326261,1.63874409819013,
9.33650440116806));
#18728=CARTESIAN_POINT('Ctrl Pts',(-0.280993269093027,1.63337857463901,
9.3391722183119));
#18729=CARTESIAN_POINT('Ctrl Pts',(-0.2971098906338,1.62776851541254,9.34184791443712));
#18730=CARTESIAN_POINT('Ctrl Pts',(-0.307118321623271,1.62428466549568,
9.34350952322718));
#18731=CARTESIAN_POINT('Ctrl Pts',(-0.317095956597471,1.62070676207948,
9.34517401751648));
#18732=CARTESIAN_POINT('Ctrl Pts',(-0.327029564295253,1.61703917202283,
9.34683953674638));
#18733=CARTESIAN_POINT('Ctrl Pts',(-0.385058843550973,1.59561416571415,
9.35656902108263));
#18734=CARTESIAN_POINT('Ctrl Pts',(-0.441695945414057,1.57109483599993,
9.36635131878856));
#18735=CARTESIAN_POINT('Ctrl Pts',(-0.496653381265967,1.54351374113654,
9.37620782348998));
#18736=CARTESIAN_POINT('Ctrl Pts',(-0.550666441336512,1.51640659338528,
9.38589495630962));
#18737=CARTESIAN_POINT('Ctrl Pts',(-0.603057746949111,1.48634144533044,
9.39565376772527));
#18738=CARTESIAN_POINT('Ctrl Pts',(-0.653517363153777,1.45331593243132,
9.40550456733641));
#18739=CARTESIAN_POINT('Ctrl Pts',(-0.702505928279116,1.4212532135455,9.4150681862179));
#18740=CARTESIAN_POINT('Ctrl Pts',(-0.749674214490309,1.38639968870215,
9.42471850800499));
#18741=CARTESIAN_POINT('Ctrl Pts',(-0.794695568814028,1.3487295473085,9.43447411731777));
#18742=CARTESIAN_POINT('Ctrl Pts',(-0.810060718838732,1.33587326204877,
9.43780356848434));
#18743=CARTESIAN_POINT('Ctrl Pts',(-0.825175397375936,1.32268873629785,
9.44114528312221));
#18744=CARTESIAN_POINT('Ctrl Pts',(-0.840025297123196,1.30917445368946,
9.4445));
#18745=CARTESIAN_POINT('',(0.0562002947523052,1.95126002955752,9.046));
#18746=CARTESIAN_POINT('Origin',(0.,0.,9.046));
#18747=CARTESIAN_POINT('Ctrl Pts',(-1.84387051712372,-0.000685899417074366,
9.15893008989225));
#18748=CARTESIAN_POINT('Ctrl Pts',(-1.84476283066793,0.0251456289795263,
9.15793473042775));
#18749=CARTESIAN_POINT('Ctrl Pts',(-1.84507215638603,0.0510244107480692,
9.15693934186537));
#18750=CARTESIAN_POINT('Ctrl Pts',(-1.84480573917948,0.0769346286138066,
9.1559436922441));
#18751=CARTESIAN_POINT('Ctrl Pts',(-1.84407856754811,0.147655193694427,
9.15322611942388));
#18752=CARTESIAN_POINT('Ctrl Pts',(-1.83907076887915,0.218209205892797,
9.15052194970773));
#18753=CARTESIAN_POINT('Ctrl Pts',(-1.83003406491836,0.288270461308813,
9.14782667059928));
#18754=CARTESIAN_POINT('Ctrl Pts',(-1.82102660530416,0.35810498631012,9.14514011388306));
#18755=CARTESIAN_POINT('Ctrl Pts',(-1.80801584752918,0.427450903626474,
9.14246239032455));
#18756=CARTESIAN_POINT('Ctrl Pts',(-1.79119418439719,0.495991519692167,
9.13978903109544));
#18757=CARTESIAN_POINT('Ctrl Pts',(-1.77853014929814,0.54759169505862,9.13777641707242));
#18758=CARTESIAN_POINT('Ctrl Pts',(-1.76370501453111,0.598735674972647,
9.13576627661749));
#18759=CARTESIAN_POINT('Ctrl Pts',(-1.74678162412797,0.649285717226304,
9.13375670293922));
#18760=CARTESIAN_POINT('Ctrl Pts',(-1.73714767088699,0.678062264466551,
9.13261271592541));
#18761=CARTESIAN_POINT('Ctrl Pts',(-1.72683345109667,0.7066462701884,9.131468912585));
#18762=CARTESIAN_POINT('Ctrl Pts',(-1.71584835159382,0.735011504504436,
9.13032494115134));
#18763=CARTESIAN_POINT('Ctrl Pts',(-1.71100614127397,0.747514844168743,
9.12982068078663));
#18764=CARTESIAN_POINT('Ctrl Pts',(-1.70603355688525,0.75997566624557,9.12931638776091));
#18765=CARTESIAN_POINT('Ctrl Pts',(-1.70093130867429,0.772391673509186,
9.12881203194595));
#18766=CARTESIAN_POINT('Ctrl Pts',(-1.69655013131485,0.783052999197183,
9.12837895378388));
#18767=CARTESIAN_POINT('Ctrl Pts',(-1.69207380809,0.79367997378185,9.12794588138746));
#18768=CARTESIAN_POINT('Ctrl Pts',(-1.68750792088798,0.804259883490199,
9.12751325944918));
#18769=CARTESIAN_POINT('Ctrl Pts',(-1.65901258128147,0.8702882601905,9.12481330027211));
#18770=CARTESIAN_POINT('Ctrl Pts',(-1.62698410576056,0.934604514869337,
9.12212599867707));
#18771=CARTESIAN_POINT('Ctrl Pts',(-1.59161919700648,0.996889483350542,
9.11944691608334));
#18772=CARTESIAN_POINT('Ctrl Pts',(-1.55617870750904,1.05930756525925,9.11676210784062));
#18773=CARTESIAN_POINT('Ctrl Pts',(-1.51738711621801,1.11968666473227,9.11408555376753));
#18774=CARTESIAN_POINT('Ctrl Pts',(-1.47539333726015,1.17769038855139,9.11141278676449));
#18775=CARTESIAN_POINT('Ctrl Pts',(-1.43413146740691,1.23468316611567,9.10878660338771));
#18776=CARTESIAN_POINT('Ctrl Pts',(-1.38977757023931,1.2893835170435,9.10616407622178));
#18777=CARTESIAN_POINT('Ctrl Pts',(-1.34243235737242,1.34144399157684,9.10354096769098));
#18778=CARTESIAN_POINT('Ctrl Pts',(-1.32721791009383,1.35817369447865,9.1026980282673));
#18779=CARTESIAN_POINT('Ctrl Pts',(-1.31169427190245,1.37463051052086,9.101855028808));
#18780=CARTESIAN_POINT('Ctrl Pts',(-1.2958639972742,1.39080204565998,9.10101182868962));
#18781=CARTESIAN_POINT('Ctrl Pts',(-1.28762458675722,1.39921907693897,9.10057295620721));
#18782=CARTESIAN_POINT('Ctrl Pts',(-1.27930873672108,1.40755201990811,9.10013438322948));
#18783=CARTESIAN_POINT('Ctrl Pts',(-1.27091852207937,1.41579817729257,9.0996961596087));
#18784=CARTESIAN_POINT('Ctrl Pts',(-1.22163456203449,1.46423594776861,9.09712204245684));
#18785=CARTESIAN_POINT('Ctrl Pts',(-1.16977311651428,1.50969609064883,9.09455919964471));
#18786=CARTESIAN_POINT('Ctrl Pts',(-1.11547064510272,1.55188751878994,9.09200378176057));
#18787=CARTESIAN_POINT('Ctrl Pts',(-1.05997608101023,1.59500516799204,9.08939226523345));
#18788=CARTESIAN_POINT('Ctrl Pts',(-1.00193205212083,1.63471019377729,9.08678850320891));
#18789=CARTESIAN_POINT('Ctrl Pts',(-0.941699156915238,1.67101078688361,
9.08418838715268));
#18790=CARTESIAN_POINT('Ctrl Pts',(-0.880245158955871,1.70804730267893,
9.08153555888884));
#18791=CARTESIAN_POINT('Ctrl Pts',(-0.816511792195639,1.74154029826807,
9.07888652592138));
#18792=CARTESIAN_POINT('Ctrl Pts',(-0.750851384302144,1.7714536219802,9.07623692473885));
#18793=CARTESIAN_POINT('Ctrl Pts',(-0.735368379689796,1.77850731146925,
9.07561213746375));
#18794=CARTESIAN_POINT('Ctrl Pts',(-0.719778125572124,1.78536175208163,
9.07498731859381));
#18795=CARTESIAN_POINT('Ctrl Pts',(-0.704085082311001,1.79201608287082,
9.07436241091651));
#18796=CARTESIAN_POINT('Ctrl Pts',(-0.689155208372567,1.79834680650256,
9.07376789316174));
#18797=CARTESIAN_POINT('Ctrl Pts',(-0.674127745726515,1.80449806819125,
9.07317311800809));
#18798=CARTESIAN_POINT('Ctrl Pts',(-0.659034674467403,1.81045829022041,
9.07257913841047));
#18799=CARTESIAN_POINT('Ctrl Pts',(-0.591575493283209,1.83709777868902,
9.0699243190826));
#18800=CARTESIAN_POINT('Ctrl Pts',(-0.522714141676951,1.85996688588042,
9.06728160073073));
#18801=CARTESIAN_POINT('Ctrl Pts',(-0.452831713589392,1.87908057169854,
9.064646767212));
#18802=CARTESIAN_POINT('Ctrl Pts',(-0.381964429865557,1.8984636273958,9.06197480088732));
#18803=CARTESIAN_POINT('Ctrl Pts',(-0.310046121550136,1.91398495893907,
9.05931094320431));
#18804=CARTESIAN_POINT('Ctrl Pts',(-0.237448384653525,1.92561288101988,
9.05665079724139));
#18805=CARTESIAN_POINT('Ctrl Pts',(-0.16509915768935,1.93720099946144,9.0539997572468));
#18806=CARTESIAN_POINT('Ctrl Pts',(-0.0920741051298766,1.94492250064192,
9.05135240360455));
#18807=CARTESIAN_POINT('Ctrl Pts',(-0.0187307257833482,1.94869601579968,
9.04870438439208));
#18808=CARTESIAN_POINT('Ctrl Pts',(0.00623373766317573,1.94998043686209,
9.04780305724539));
#18809=CARTESIAN_POINT('Ctrl Pts',(0.0312350991919573,1.95080701502899,
9.04690165298766));
#18810=CARTESIAN_POINT('Ctrl Pts',(0.0562592026297113,1.95117115182352,
9.046));
#18811=CARTESIAN_POINT('',(-1.,-1.22464679914735E-16,10.));
#18812=CARTESIAN_POINT('',(-1.5,-1.83697019872103E-16,9.5));
#18813=CARTESIAN_POINT('Origin',(0.,0.,10.));
#18814=CARTESIAN_POINT('Ctrl Pts',(1.13509973994372,-1.59049193030952,-0.230074082272068));
#18815=CARTESIAN_POINT('Ctrl Pts',(1.6638518199518,-1.21313299055364,-0.193036827370107));
#18816=CARTESIAN_POINT('Ctrl Pts',(2.3063342838214,0.103787718385998,-0.118962317566186));
#18817=CARTESIAN_POINT('Ctrl Pts',(1.16188726092372,1.99754004216699,-0.0078505528603034));
#18818=CARTESIAN_POINT('Ctrl Pts',(-1.04656155408942,2.05782827558088,0.103261211845579));
#18819=CARTESIAN_POINT('Ctrl Pts',(-2.29698247648793,0.238323790666827,
0.214372976551461));
#18820=CARTESIAN_POINT('Ctrl Pts',(-1.44612258918391,-1.80076047995977,
0.325484741257344));
#18821=CARTESIAN_POINT('Ctrl Pts',(0.727960807006611,-2.19149445634993,
0.436596505963226));
#18822=CARTESIAN_POINT('Ctrl Pts',(2.23594625441705,-0.57761383484556,0.547708270669108));
#18823=CARTESIAN_POINT('Ctrl Pts',(1.69826458517493,1.56495710236821,0.658820035374991));
#18824=CARTESIAN_POINT('Ctrl Pts',(-0.393209187557514,2.27560539746713,
0.769931800080872));
#18825=CARTESIAN_POINT('Ctrl Pts',(-2.1249183445612,0.904323940984954,0.881043564786756));
#18826=CARTESIAN_POINT('Ctrl Pts',(-1.91250851401755,-1.29437122529363,
0.992155329492637));
#18827=CARTESIAN_POINT('Ctrl Pts',(0.0496914524290519,-2.30880688864344,
1.10326709419852));
#18828=CARTESIAN_POINT('Ctrl Pts',(1.96642629593332,-1.21088396446372,1.2143788589044));
#18829=CARTESIAN_POINT('Ctrl Pts',(2.08404446099042,0.994902325724329,1.32549062361028));
#18830=CARTESIAN_POINT('Ctrl Pts',(0.294933807152522,2.29043279904655,1.43660238831617));
#18831=CARTESIAN_POINT('Ctrl Pts',(-1.76401667284967,1.49040789535707,1.54771415302205));
#18832=CARTESIAN_POINT('Ctrl Pts',(-2.20903784902227,-0.673217691022686,
1.65882591772793));
#18833=CARTESIAN_POINT('Ctrl Pts',(-0.632971955670129,-2.22090439277293,
1.76993768243381));
#18834=CARTESIAN_POINT('Ctrl Pts',(1.52221091586757,-1.73664736597321,1.8810494471397));
#18835=CARTESIAN_POINT('Ctrl Pts',(2.28469665983849,0.336498526979157,1.99216121184558));
#18836=CARTESIAN_POINT('Ctrl Pts',(0.956873830222989,2.10177603540478,2.10327297655146));
#18837=CARTESIAN_POINT('Ctrl Pts',(-1.24640944320213,1.94410225513366,2.21438474125735));
#18838=CARTESIAN_POINT('Ctrl Pts',(-2.30933112102653,0.0077356190240744,
2.32549650596323));
#18839=CARTESIAN_POINT('Ctrl Pts',(-1.25940573752146,-1.93570846156897,
2.43660827066911));
#18840=CARTESIAN_POINT('Ctrl Pts',(0.942771778257433,-2.10813933150712,
2.54772003537499));
#18841=CARTESIAN_POINT('Ctrl Pts',(2.28239105758209,-0.351796993969821,
2.65883180008088));
#18842=CARTESIAN_POINT('Ctrl Pts',(1.5338112075673,1.72641050841568,2.76994356478675));
#18843=CARTESIAN_POINT('Ctrl Pts',(-0.618079094904134,2.22509512099281,
2.88105532949264));
#18844=CARTESIAN_POINT('Ctrl Pts',(-2.20447812307392,0.688001649364983,
2.99216709419852));
#18845=CARTESIAN_POINT('Ctrl Pts',(-1.77396191596644,-1.47855645319501,
3.1032788589044));
#18846=CARTESIAN_POINT('Ctrl Pts',(0.279582788264576,-2.29235763554206,
3.21439062361029));
#18847=CARTESIAN_POINT('Ctrl Pts',(2.07733235475043,-1.00884109381303,3.32550238831616));
#18848=CARTESIAN_POINT('Ctrl Pts',(1.97449455267563,1.19768164639481,3.43661415302206));
#18849=CARTESIAN_POINT('Ctrl Pts',(0.0651574691963124,2.30842469421968,
3.54772591772793));
#18850=CARTESIAN_POINT('Ctrl Pts',(-1.90379331193745,1.30714998760185,3.65883768243382));
#18851=CARTESIAN_POINT('Ctrl Pts',(-2.13093060196669,-0.890058893707459,
3.7699494471397));
#18852=CARTESIAN_POINT('Ctrl Pts',(-0.408442558280485,-2.27293746971921,
3.88106121184558));
#18853=CARTESIAN_POINT('Ctrl Pts',(1.68773665970145,-1.57626616793184,3.99217297655146));
#18854=CARTESIAN_POINT('Ctrl Pts',(2.23977636166251,0.562558365331801,4.10328474125734));
#18855=CARTESIAN_POINT('Ctrl Pts',(0.74260585822099,2.18668850182259,4.21439650596323));
#18856=CARTESIAN_POINT('Ctrl Pts',(-1.43398761320325,1.81017943581477,4.32550827066911));
#18857=CARTESIAN_POINT('Ctrl Pts',(-2.29860096835557,-0.222494163837853,
4.43662003537499));
#18858=CARTESIAN_POINT('Ctrl Pts',(-1.06018446609557,-2.05160399748995,
4.54773180008088));
#18859=CARTESIAN_POINT('Ctrl Pts',(1.14821317567414,-2.00366578247853,4.65884356478675));
#18860=CARTESIAN_POINT('Ctrl Pts',(2.30609068612924,-0.122539022418222,
4.76995532949264));
#18861=CARTESIAN_POINT('Ctrl Pts',(1.35408586659467,1.87070081267837,4.88106709419852));
#18862=CARTESIAN_POINT('Ctrl Pts',(-0.836795576656505,2.15240405768872,
4.99217885890441));
#18863=CARTESIAN_POINT('Ctrl Pts',(-2.26207824635583,0.464835532239094,
5.10329062361028));
#18864=CARTESIAN_POINT('Ctrl Pts',(-1.61774632988599,-1.64801907659051,
5.21440238831616));
#18865=CARTESIAN_POINT('Ctrl Pts',(0.506689737022565,-2.25307247443603,
5.32551415302206));
#18866=CARTESIAN_POINT('Ctrl Pts',(2.16754658332471,-0.796750822900503,
5.43662591772793));
#18867=CARTESIAN_POINT('Ctrl Pts',(1.84527750005797,1.38853196305901,5.54773768243382));
#18868=CARTESIAN_POINT('Ctrl Pts',(-0.165267944017207,2.30342279474246,
5.65884944713968));
#18869=CARTESIAN_POINT('Ctrl Pts',(-2.02460688227655,1.11087219650157,5.76996121184559));
#18870=CARTESIAN_POINT('Ctrl Pts',(-2.03159790035992,-1.09803462415223,
5.88107297655145));
#18871=CARTESIAN_POINT('Ctrl Pts',(-0.179844794802175,-2.30233053978421,
5.99218474125735));
#18872=CARTESIAN_POINT('Ctrl Pts',(1.83645143012731,-1.40018434850804,6.10329650596322));
#18873=CARTESIAN_POINT('Ctrl Pts',(2.17254641826527,0.783014766469867,6.21440827066911));
#18874=CARTESIAN_POINT('Ctrl Pts',(0.520941041773343,2.24982010296223,6.32552003537499));
#18875=CARTESIAN_POINT('Ctrl Pts',(-1.60728232206565,1.65822604131681,6.43663180008087));
#18876=CARTESIAN_POINT('Ctrl Pts',(-2.26497523551502,-0.450507760638336,
6.54774356478676));
#18877=CARTESIAN_POINT('Ctrl Pts',(-0.850403061079838,-2.14706420492014,
6.65885532949263));
#18878=CARTESIAN_POINT('Ctrl Pts',(1.34221761756673,-1.87923440411587,6.76996709419852));
#18879=CARTESIAN_POINT('Ctrl Pts',(2.30682012517322,0.107939520395821,6.8810788589044));
#18880=CARTESIAN_POINT('Ctrl Pts',(1.16087295306313,1.99635770166139,6.99219062361028));
#18881=CARTESIAN_POINT('Ctrl Pts',(-1.04717705090239,2.05827363831718,7.10330238831617));
#18882=CARTESIAN_POINT('Ctrl Pts',(-2.29714652812405,0.237039336040665,
7.21441415302205));
#18883=CARTESIAN_POINT('Ctrl Pts',(-1.44541702482095,-1.80106632367513,
7.32552591772793));
#18884=CARTESIAN_POINT('Ctrl Pts',(0.728749912475137,-2.19134526757008,
7.43663768243382));
#18885=CARTESIAN_POINT('Ctrl Pts',(2.23617025832252,-0.576724313119789,
7.54774944713969));
#18886=CARTESIAN_POINT('Ctrl Pts',(1.69768095784581,1.56555144229893,7.65886121184558));
#18887=CARTESIAN_POINT('Ctrl Pts',(-0.394048492723434,2.27547756264829,
7.76997297655146));
#18888=CARTESIAN_POINT('Ctrl Pts',(-2.1252515343864,0.903528862339296,7.88108474125734));
#18889=CARTESIAN_POINT('Ctrl Pts',(-1.91203390686379,-1.29507220804901,
7.99219650596323));
#18890=CARTESIAN_POINT('Ctrl Pts',(0.0505534074973998,-2.30879278288063,
8.10330827066911));
#18891=CARTESIAN_POINT('Ctrl Pts',(1.9668566708909,-1.21015215007583,8.21442003537499));
#18892=CARTESIAN_POINT('Ctrl Pts',(2.08370935603324,0.995664930130442,8.32553180008088));
#18893=CARTESIAN_POINT('Ctrl Pts',(0.294024709520203,2.2905551434179,8.43664356478675));
#18894=CARTESIAN_POINT('Ctrl Pts',(-1.76444823276047,1.48973062083675,8.54775532949265));
#18895=CARTESIAN_POINT('Ctrl Pts',(-2.20901589213136,-0.673986377788178,
8.65886709419851));
#18896=CARTESIAN_POINT('Ctrl Pts',(-0.631718430347985,-2.22122906321008,
8.76997885890441));
#18897=CARTESIAN_POINT('Ctrl Pts',(1.52202596973473,-1.73591049473505,8.88109062361028));
#18898=CARTESIAN_POINT('Ctrl Pts',(2.28617112150847,0.33700123195322,8.99220238831617));
#18899=CARTESIAN_POINT('Ctrl Pts',(0.952838501929636,2.10286673578195,9.10331415302205));
#18900=CARTESIAN_POINT('Ctrl Pts',(-0.508499740558942,1.99537528935738,
9.17738866282597));
#18901=CARTESIAN_POINT('Ctrl Pts',(-1.05522946356713,1.64456887335855,9.21442591772793));
#18902=CARTESIAN_POINT('Ctrl Pts',(1.05793541951255,-1.48236995244729,-0.153382721514713));
#18903=CARTESIAN_POINT('Ctrl Pts',(1.55074282127375,-1.13066395323947,-0.116345466612752));
#18904=CARTESIAN_POINT('Ctrl Pts',(2.14954919134395,0.0967322073357151,
-0.0422709568088308));
#18905=CARTESIAN_POINT('Ctrl Pts',(1.08290191914989,1.86174684755704,0.0688408078970521));
#18906=CARTESIAN_POINT('Ctrl Pts',(-0.975416078261274,1.91793667411056,
0.179952572602934));
#18907=CARTESIAN_POINT('Ctrl Pts',(-2.14083312185121,0.222122488964202,
0.291064337308817));
#18908=CARTESIAN_POINT('Ctrl Pts',(-1.34781486967012,-1.67834440161383,
0.402176102014699));
#18909=CARTESIAN_POINT('Ctrl Pts',(0.678473877359381,-2.04251619963627,
0.513287866720582));
#18910=CARTESIAN_POINT('Ctrl Pts',(2.08394615506782,-0.538347524168997,
0.624399631426463));
#18911=CARTESIAN_POINT('Ctrl Pts',(1.5828161994376,1.45857098751088,0.735511396132347));
#18912=CARTESIAN_POINT('Ctrl Pts',(-0.366478743811078,2.12090926118418,
0.846623160838227));
#18913=CARTESIAN_POINT('Ctrl Pts',(-1.98046594600992,0.842847808183427,
0.957734925544112));
#18914=CARTESIAN_POINT('Ctrl Pts',(-1.78249578067807,-1.20637959559737,
1.06884669024999));
#18915=CARTESIAN_POINT('Ctrl Pts',(0.0463134169816076,-2.15185370796715,
1.17995845495588));
#18916=CARTESIAN_POINT('Ctrl Pts',(1.83274822037389,-1.12856781641888,1.29107021966175));
#18917=CARTESIAN_POINT('Ctrl Pts',(1.9423706776904,0.927268655168022,1.40218198436764));
#18918=CARTESIAN_POINT('Ctrl Pts',(0.274884144554374,2.13472869286777,1.51329374907352));
#18919=CARTESIAN_POINT('Ctrl Pts',(-1.64409844628356,1.38908965136187,1.62440551377941));
#18920=CARTESIAN_POINT('Ctrl Pts',(-2.05886698876376,-0.627452209979957,
1.73551727848529));
#18921=CARTESIAN_POINT('Ctrl Pts',(-0.589942388229901,-2.06992684236011,
1.84662904319117));
#18922=CARTESIAN_POINT('Ctrl Pts',(1.41873069581074,-1.61858971067802,1.95774080789705));
#18923=CARTESIAN_POINT('Ctrl Pts',(2.12938249761644,0.313623285934951,2.06885257260293));
#18924=CARTESIAN_POINT('Ctrl Pts',(0.891825344835078,1.95889685592529,2.17996433730882));
#18925=CARTESIAN_POINT('Ctrl Pts',(-1.1616782655979,1.81194177259002,2.2910761020147));
#18926=CARTESIAN_POINT('Ctrl Pts',(-2.15234230292194,0.00720975000647539,
2.40218786672058));
#18927=CARTESIAN_POINT('Ctrl Pts',(-1.17379106908025,-1.80411859088743,
2.51329963142647));
#18928=CARTESIAN_POINT('Ctrl Pts',(0.878681953345199,-1.96482757381254,
2.62441139613234));
#18929=CARTESIAN_POINT('Ctrl Pts',(2.12723363068914,-0.327881759903454,
2.73552316083823));
#18930=CARTESIAN_POINT('Ctrl Pts',(1.42954239722687,1.60904875686269,2.84663492554411));
#18931=CARTESIAN_POINT('Ctrl Pts',(-0.576061947289118,2.07383268398912,
2.95774669024999));
#18932=CARTESIAN_POINT('Ctrl Pts',(-2.05461723394991,0.641231151706844,
3.06885845495588));
#18933=CARTESIAN_POINT('Ctrl Pts',(-1.6533676096695,-1.37804387274497,3.17997021966176));
#18934=CARTESIAN_POINT('Ctrl Pts',(0.260576691177686,-2.13652267857115,
3.29108198436765));
#18935=CARTESIAN_POINT('Ctrl Pts',(1.93611486185244,-0.94025986285354,3.40219374907351));
#18936=CARTESIAN_POINT('Ctrl Pts',(1.84026799531615,1.11626299472502,3.51330551377941));
#18937=CARTESIAN_POINT('Ctrl Pts',(0.0607280506574504,2.15149749520116,
3.62441727848528));
#18938=CARTESIAN_POINT('Ctrl Pts',(-1.77437303987893,1.21828965494074,3.73552904319117));
#18939=CARTESIAN_POINT('Ctrl Pts',(-1.98606948888519,-0.829552501837387,
3.84664080789705));
#18940=CARTESIAN_POINT('Ctrl Pts',(-0.380676546769933,-2.11842269972892,
3.95775257260293));
#18941=CARTESIAN_POINT('Ctrl Pts',(1.57300396456481,-1.46911126040525,4.06886433730882));
#18942=CARTESIAN_POINT('Ctrl Pts',(2.08751589081254,0.524315528657517,4.1799761020147));
#18943=CARTESIAN_POINT('Ctrl Pts',(0.692123354894286,2.03803695491432,4.29108786672059));
#18944=CARTESIAN_POINT('Ctrl Pts',(-1.33650483192358,1.68712305485737,4.40219963142646));
#18945=CARTESIAN_POINT('Ctrl Pts',(-2.14234158829933,-0.207368963515553,
4.51331139613235));
#18946=CARTESIAN_POINT('Ctrl Pts',(-0.988112901827546,-1.9121355237609,
4.62442316083823));
#18947=CARTESIAN_POINT('Ctrl Pts',(1.07015740110811,-1.86745615874641,4.73553492554411));
#18948=CARTESIAN_POINT('Ctrl Pts',(2.14932215347443,-0.114208793753307,
4.84664669024999));
#18949=CARTESIAN_POINT('Ctrl Pts',(1.2620348229512,1.7435301757196,4.95775845495587));
#18950=CARTESIAN_POINT('Ctrl Pts',(-0.779910036346446,2.00608317454491,
5.06887021966176));
#18951=CARTESIAN_POINT('Ctrl Pts',(-2.10830168866686,0.433235914429924,
5.17998198436764));
#18952=CARTESIAN_POINT('Ctrl Pts',(-1.50777159217538,-1.53598639115529,
5.29109374907352));
#18953=CARTESIAN_POINT('Ctrl Pts',(0.472244861518737,-2.09990813102716,
5.40220551377941));
#18954=CARTESIAN_POINT('Ctrl Pts',(2.02019630808506,-0.742587533421502,
5.51331727848529));
#18955=CARTESIAN_POINT('Ctrl Pts',(1.71983514526896,1.29413926649146,5.62442904319117));
#18956=CARTESIAN_POINT('Ctrl Pts',(-0.154032994223487,2.14683562590847,
5.73554080789705));
#18957=CARTESIAN_POINT('Ctrl Pts',(-1.88697367815045,1.03535486959847,5.84665257260293));
#18958=CARTESIAN_POINT('Ctrl Pts',(-1.89348944534568,-1.02338999813302,
5.95776433730882));
#18959=CARTESIAN_POINT('Ctrl Pts',(-0.1676189076086,-2.14581762267332,6.06887610201469));
#18960=CARTESIAN_POINT('Ctrl Pts',(1.7116090734392,-1.3049995203128,6.17998786672059));
#18961=CARTESIAN_POINT('Ctrl Pts',(2.02485625318872,0.729785257012656,6.29109963142646));
#18962=CARTESIAN_POINT('Ctrl Pts',(0.485527359557932,2.09687685645413,6.40221139613235));
#18963=CARTESIAN_POINT('Ctrl Pts',(-1.49801892982015,1.54549948426039,6.51332316083823));
#18964=CARTESIAN_POINT('Ctrl Pts',(-2.11100173989019,-0.419882147773394,
6.62443492554411));
#18965=CARTESIAN_POINT('Ctrl Pts',(-0.792592481100246,-2.0011063260971,
6.73554669024999));
#18966=CARTESIAN_POINT('Ctrl Pts',(1.25097338000271,-1.75148365180605,6.84665845495587));
#18967=CARTESIAN_POINT('Ctrl Pts',(2.15000200509789,0.100601768966674,6.95777021966176));
#18968=CARTESIAN_POINT('Ctrl Pts',(1.08195656415223,1.86064488280912,7.06888198436763));
#18969=CARTESIAN_POINT('Ctrl Pts',(-0.975989733470706,1.91835176099384,
7.17999374907353));
#18970=CARTESIAN_POINT('Ctrl Pts',(-2.14098602122241,0.220925351835228,
7.2911055137794));
#18971=CARTESIAN_POINT('Ctrl Pts',(-1.3471572697218,-1.67862945400872,7.40221727848529));
#18972=CARTESIAN_POINT('Ctrl Pts',(0.679209339271233,-2.04237715274123,
7.51332904319116));
#18973=CARTESIAN_POINT('Ctrl Pts',(2.08415493114041,-0.537518472318304,
7.62444080789706));
#18974=CARTESIAN_POINT('Ctrl Pts',(1.58227224721776,1.45912492408739,7.73555257260292));
#18975=CARTESIAN_POINT('Ctrl Pts',(-0.36726099283428,2.12079011660337,7.84666433730883));
#18976=CARTESIAN_POINT('Ctrl Pts',(-1.98077648552032,0.842106779152281,
7.95777610201469));
#18977=CARTESIAN_POINT('Ctrl Pts',(-1.78205343741902,-1.20703292539676,
8.0688878667206));
#18978=CARTESIAN_POINT('Ctrl Pts',(0.047116776162082,-2.15184056111708,
8.17999963142645));
#18979=CARTESIAN_POINT('Ctrl Pts',(1.83314933835081,-1.12788575092788,8.29111139613235));
#18980=CARTESIAN_POINT('Ctrl Pts',(1.9420583532391,0.92797941756529,8.40222316083823));
#18981=CARTESIAN_POINT('Ctrl Pts',(0.2740368475714,2.13484272024287,8.51333492554411));
#18982=CARTESIAN_POINT('Ctrl Pts',(-1.64450066866033,1.38845841810671,8.62444669025));
#18983=CARTESIAN_POINT('Ctrl Pts',(-2.05884652450694,-0.62816864125653,
8.73555845495587));
#18984=CARTESIAN_POINT('Ctrl Pts',(-0.588774077824317,-2.07022944163225,
8.84667021966176));
#18985=CARTESIAN_POINT('Ctrl Pts',(1.41855832235513,-1.61790293210251,8.95778198436763));
#18986=CARTESIAN_POINT('Ctrl Pts',(2.1307567250702,0.31409181691854,9.06889374907353));
#18987=CARTESIAN_POINT('Ctrl Pts',(0.888064339012712,1.9599134102601,9.1800055137794));
#18988=CARTESIAN_POINT('Ctrl Pts',(-0.473931820631839,1.85972925510133,
9.25408002358333));
#18989=CARTESIAN_POINT('Ctrl Pts',(-0.983494741419154,1.53277073346885,
9.29111727848529));
#18990=CARTESIAN_POINT('Ctrl Pts',(0.980771099081378,-1.37424797458506,
-0.0766913607573575));
#18991=CARTESIAN_POINT('Ctrl Pts',(1.43763382259569,-1.0481949159253,-0.0396541058553967));
#18992=CARTESIAN_POINT('Ctrl Pts',(1.99276409886649,0.0896766962854344,
0.0344204039485245));
#18993=CARTESIAN_POINT('Ctrl Pts',(1.00391657737607,1.72595365294709,0.145532168654408));
#18994=CARTESIAN_POINT('Ctrl Pts',(-0.904270602433131,1.77804507264024,
0.256643933360289));
#18995=CARTESIAN_POINT('Ctrl Pts',(-1.9846837672145,0.205921187261574,0.367755698066172));
#18996=CARTESIAN_POINT('Ctrl Pts',(-1.24950715015633,-1.55592832326788,
0.478867462772054));
#18997=CARTESIAN_POINT('Ctrl Pts',(0.628986947712151,-1.89353794292261,
0.589979227477937));
#18998=CARTESIAN_POINT('Ctrl Pts',(1.93194605571859,-0.499081213492431,
0.701090992183818));
#18999=CARTESIAN_POINT('Ctrl Pts',(1.46736781370027,1.35218487265355,0.812202756889702));
#19000=CARTESIAN_POINT('Ctrl Pts',(-0.339748300064645,1.96621312490123,
0.923314521595583));
#19001=CARTESIAN_POINT('Ctrl Pts',(-1.83601354745863,0.781371675381896,
1.03442628630147));
#19002=CARTESIAN_POINT('Ctrl Pts',(-1.65248304733859,-1.11838796590112,
1.14553805100735));
#19003=CARTESIAN_POINT('Ctrl Pts',(0.0429353815341671,-1.99490052729086,
1.25664981571323));
#19004=CARTESIAN_POINT('Ctrl Pts',(1.69907014481445,-1.04625166837404,1.36776158041911));
#19005=CARTESIAN_POINT('Ctrl Pts',(1.80069689439038,0.859634984611714,1.47887334512499));
#19006=CARTESIAN_POINT('Ctrl Pts',(0.254834481956223,1.97902458668898,1.58998510983088));
#19007=CARTESIAN_POINT('Ctrl Pts',(-1.52418021971745,1.28777140736668,1.70109687453676));
#19008=CARTESIAN_POINT('Ctrl Pts',(-1.90869612850525,-0.58168672893723,
1.81220863924264));
#19009=CARTESIAN_POINT('Ctrl Pts',(-0.546912820789672,-1.91894929194728,
1.92332040394852));
#19010=CARTESIAN_POINT('Ctrl Pts',(1.3152504757539,-1.50053205538284,2.03443216865441));
#19011=CARTESIAN_POINT('Ctrl Pts',(1.97406833539439,0.290748044890748,2.14554393336029));
#19012=CARTESIAN_POINT('Ctrl Pts',(0.826776859447168,1.8160176764458,2.25665569806617));
#19013=CARTESIAN_POINT('Ctrl Pts',(-1.07694708799367,1.67978129004639,2.36776746277206));
#19014=CARTESIAN_POINT('Ctrl Pts',(-1.99535348481736,0.00668388098887723,
2.47887922747793));
#19015=CARTESIAN_POINT('Ctrl Pts',(-1.08817640063904,-1.67252872020589,
2.58999099218382));
#19016=CARTESIAN_POINT('Ctrl Pts',(0.814592128432962,-1.82151581611796,
2.70110275688969));
#19017=CARTESIAN_POINT('Ctrl Pts',(1.97207620379619,-0.303966525837088,
2.81221452159559));
#19018=CARTESIAN_POINT('Ctrl Pts',(1.32527358688643,1.49168700530971,2.92332628630146));
#19019=CARTESIAN_POINT('Ctrl Pts',(-0.5340447996741,1.92257024698542,3.03443805100735));
#19020=CARTESIAN_POINT('Ctrl Pts',(-1.9047563448259,0.594460654048706,3.14554981571323));
#19021=CARTESIAN_POINT('Ctrl Pts',(-1.53277330337256,-1.27753129229492,
3.25666158041911));
#19022=CARTESIAN_POINT('Ctrl Pts',(0.241570594090793,-1.98068772160023,
3.367773345125));
#19023=CARTESIAN_POINT('Ctrl Pts',(1.79489736895445,-0.871678631894047,
3.47888510983087));
#19024=CARTESIAN_POINT('Ctrl Pts',(1.70604143795667,1.03484434305524,3.58999687453676));
#19025=CARTESIAN_POINT('Ctrl Pts',(0.0562986321185907,1.99457029618264,
3.70110863924264));
#19026=CARTESIAN_POINT('Ctrl Pts',(-1.64495276782042,1.12942932227964,3.81222040394853));
#19027=CARTESIAN_POINT('Ctrl Pts',(-1.84120837580369,-0.769046109967315,
3.92333216865441));
#19028=CARTESIAN_POINT('Ctrl Pts',(-0.352910535259385,-1.96390792973863,
4.03444393336029));
#19029=CARTESIAN_POINT('Ctrl Pts',(1.45827126942817,-1.36195635287866,4.14555569806618));
#19030=CARTESIAN_POINT('Ctrl Pts',(1.93525541996257,0.486072691983231,4.25666746277205));
#19031=CARTESIAN_POINT('Ctrl Pts',(0.641640851567584,1.88938540800605,4.36777922747794));
#19032=CARTESIAN_POINT('Ctrl Pts',(-1.2390220506439,1.56406667389998,4.47889099218382));
#19033=CARTESIAN_POINT('Ctrl Pts',(-1.98608220824309,-0.192243763193254,
4.5900027568897));
#19034=CARTESIAN_POINT('Ctrl Pts',(-0.916041337559525,-1.77266705003184,
4.70111452159558));
#19035=CARTESIAN_POINT('Ctrl Pts',(0.992101626542076,-1.73124653501428,
4.81222628630146));
#19036=CARTESIAN_POINT('Ctrl Pts',(1.99255362081962,-0.105878565088393,
4.92333805100735));
#19037=CARTESIAN_POINT('Ctrl Pts',(1.16998377930773,1.61635953876083,5.03444981571323));
#19038=CARTESIAN_POINT('Ctrl Pts',(-0.72302449603639,1.85976229140111,5.14556158041912));
#19039=CARTESIAN_POINT('Ctrl Pts',(-1.95452513097788,0.401636296620756,
5.25667334512499));
#19040=CARTESIAN_POINT('Ctrl Pts',(-1.39779685446476,-1.42395370572007,
5.36778510983088));
#19041=CARTESIAN_POINT('Ctrl Pts',(0.43779998601491,-1.9467437876183,5.47889687453675));
#19042=CARTESIAN_POINT('Ctrl Pts',(1.8728460328454,-0.688424243942499,5.59000863924265));
#19043=CARTESIAN_POINT('Ctrl Pts',(1.59439279047996,1.19974656992392,5.70112040394852));
#19044=CARTESIAN_POINT('Ctrl Pts',(-0.142798044429764,1.99024845707447,
5.81223216865441));
#19045=CARTESIAN_POINT('Ctrl Pts',(-1.74934047402436,0.959837542695381,
5.92334393336029));
#19046=CARTESIAN_POINT('Ctrl Pts',(-1.75538099033144,-0.948745372113812,
6.03445569806617));
#19047=CARTESIAN_POINT('Ctrl Pts',(-0.155393020415026,-1.98930470556244,
6.14556746277206));
#19048=CARTESIAN_POINT('Ctrl Pts',(1.58676671675109,-1.20981469211756,6.25667922747794));
#19049=CARTESIAN_POINT('Ctrl Pts',(1.87716608811217,0.676555747555444,6.36779099218382));
#19050=CARTESIAN_POINT('Ctrl Pts',(0.45011367734252,1.94393360994604,6.4789027568897));
#19051=CARTESIAN_POINT('Ctrl Pts',(-1.38875553757466,1.43277292720395,6.59001452159559));
#19052=CARTESIAN_POINT('Ctrl Pts',(-1.95702824426536,-0.389256534908447,
6.70112628630146));
#19053=CARTESIAN_POINT('Ctrl Pts',(-0.734781901120652,-1.85514844727406,
6.81223805100735));
#19054=CARTESIAN_POINT('Ctrl Pts',(1.15972914243869,-1.62373289949622,6.92334981571322));
#19055=CARTESIAN_POINT('Ctrl Pts',(1.99318388502257,0.0932640175375246,
7.03446158041912));
#19056=CARTESIAN_POINT('Ctrl Pts',(1.00304017524133,1.72493206395685,7.14557334512499));
#19057=CARTESIAN_POINT('Ctrl Pts',(-0.904802416039021,1.7784298836705,7.25668510983089));
#19058=CARTESIAN_POINT('Ctrl Pts',(-1.98482551432077,0.20481136762979,7.36779687453676));
#19059=CARTESIAN_POINT('Ctrl Pts',(-1.24889751462265,-1.55619258434231,
7.47890863924264));
#19060=CARTESIAN_POINT('Ctrl Pts',(0.62966876606733,-1.89340903791239,7.59002040394853));
#19061=CARTESIAN_POINT('Ctrl Pts',(1.93213960395831,-0.498312631516818,
7.7011321686544));
#19062=CARTESIAN_POINT('Ctrl Pts',(1.46686353658972,1.35269840587584,7.8122439333603));
#19063=CARTESIAN_POINT('Ctrl Pts',(-0.340473492945126,1.96610267055844,
7.92335569806617));
#19064=CARTESIAN_POINT('Ctrl Pts',(-1.83630143665424,0.780684695965268,
8.03446746277206));
#19065=CARTESIAN_POINT('Ctrl Pts',(-1.65207296797424,-1.11899364274452,
8.14557922747793));
#19066=CARTESIAN_POINT('Ctrl Pts',(0.043680144826762,-1.99488833935353,
8.25669099218383));
#19067=CARTESIAN_POINT('Ctrl Pts',(1.69944200581072,-1.04561935177993,8.36780275688969));
#19068=CARTESIAN_POINT('Ctrl Pts',(1.80040735044495,0.860293905000138,8.47891452159559));
#19069=CARTESIAN_POINT('Ctrl Pts',(0.2540489856226,1.97913029706784,8.59002628630146));
#19070=CARTESIAN_POINT('Ctrl Pts',(-1.52455310456019,1.28718621537667,8.70113805100735));
#19071=CARTESIAN_POINT('Ctrl Pts',(-1.90867715688251,-0.58235090472488,
8.81224981571322));
#19072=CARTESIAN_POINT('Ctrl Pts',(-0.54582972530065,-1.91922982005443,
8.92336158041912));
#19073=CARTESIAN_POINT('Ctrl Pts',(1.31509067497552,-1.49989536946997,9.03447334512499));
#19074=CARTESIAN_POINT('Ctrl Pts',(1.97534232863193,0.291182401883861,9.14558510983087));
#19075=CARTESIAN_POINT('Ctrl Pts',(0.823290176095783,1.81696008473825,9.25669687453676));
#19076=CARTESIAN_POINT('Ctrl Pts',(-0.439363900704735,1.72408322084529,
9.33077138434068));
#19077=CARTESIAN_POINT('Ctrl Pts',(-0.911760019271175,1.42097259357916,
9.36780863924264));
#19078=CARTESIAN_POINT('Ctrl Pts',(0.903606778650207,-1.26612599672284,
-2.22044604925031E-15));
#19079=CARTESIAN_POINT('Ctrl Pts',(1.32452482391764,-0.965725878611127,
0.0370372549019586));
#19080=CARTESIAN_POINT('Ctrl Pts',(1.83597900638904,0.0826211852351528,
0.11111176470588));
#19081=CARTESIAN_POINT('Ctrl Pts',(0.924931235602245,1.59016045833715,0.222223529411763));
#19082=CARTESIAN_POINT('Ctrl Pts',(-0.83312512660499,1.63815347116992,0.333335294117645));
#19083=CARTESIAN_POINT('Ctrl Pts',(-1.82853441257778,0.189719885558947,
0.444447058823527));
#19084=CARTESIAN_POINT('Ctrl Pts',(-1.15119943064254,-1.43351224492194,
0.55555882352941));
#19085=CARTESIAN_POINT('Ctrl Pts',(0.579500018064921,-1.74455968620895,
0.666670588235291));
#19086=CARTESIAN_POINT('Ctrl Pts',(1.77994595636936,-0.459814902815864,
0.777782352941175));
#19087=CARTESIAN_POINT('Ctrl Pts',(1.35191942796293,1.24579875779621,0.888894117647056));
#19088=CARTESIAN_POINT('Ctrl Pts',(-0.31301785631821,1.81151698861828,1.00000588235294));
#19089=CARTESIAN_POINT('Ctrl Pts',(-1.69156114890735,0.719895542580366,
1.11111764705882));
#19090=CARTESIAN_POINT('Ctrl Pts',(-1.52247031399911,-1.03039633620486,
1.2222294117647));
#19091=CARTESIAN_POINT('Ctrl Pts',(0.0395573460867233,-1.83794734661457,
1.33334117647059));
#19092=CARTESIAN_POINT('Ctrl Pts',(1.56539206925502,-0.963935520329204,
1.44445294117647));
#19093=CARTESIAN_POINT('Ctrl Pts',(1.65902311109036,0.792001314055404,1.55556470588235));
#19094=CARTESIAN_POINT('Ctrl Pts',(0.234784819358076,1.82332048051019,1.66667647058823));
#19095=CARTESIAN_POINT('Ctrl Pts',(-1.40426199315134,1.18645316337148,1.77778823529412));
#19096=CARTESIAN_POINT('Ctrl Pts',(-1.75852526824674,-0.535921247894501,
1.88889999999999));
#19097=CARTESIAN_POINT('Ctrl Pts',(-0.503883253349445,-1.76797174153445,
2.00001176470588));
#19098=CARTESIAN_POINT('Ctrl Pts',(1.21177025569706,-1.38247440008765,2.11112352941176));
#19099=CARTESIAN_POINT('Ctrl Pts',(1.81875417317235,0.267872803846544,2.22223529411764));
#19100=CARTESIAN_POINT('Ctrl Pts',(0.761728374059259,1.67313849696631,2.33334705882353));
#19101=CARTESIAN_POINT('Ctrl Pts',(-0.992215910389441,1.54762080750275,
2.44445882352941));
#19102=CARTESIAN_POINT('Ctrl Pts',(-1.83836466671278,0.00615801197127806,
2.55557058823529));
#19103=CARTESIAN_POINT('Ctrl Pts',(-1.00256173219784,-1.54093884952435,
2.66668235294118));
#19104=CARTESIAN_POINT('Ctrl Pts',(0.750502303520728,-1.67820405842339,
2.77779411764705));
#19105=CARTESIAN_POINT('Ctrl Pts',(1.81691877690325,-0.280051291770722,
2.88890588235294));
#19106=CARTESIAN_POINT('Ctrl Pts',(1.221004776546,1.37432525375672,3.00001764705882));
#19107=CARTESIAN_POINT('Ctrl Pts',(-0.492027652059084,1.77130780998173,
3.11112941176471));
#19108=CARTESIAN_POINT('Ctrl Pts',(-1.75489545570189,0.547690156390568,
3.22224117647059));
#19109=CARTESIAN_POINT('Ctrl Pts',(-1.41217899707562,-1.17701871184488,
3.33335294117647));
#19110=CARTESIAN_POINT('Ctrl Pts',(0.2225644970039,-1.82485276462931,3.44446470588235));
#19111=CARTESIAN_POINT('Ctrl Pts',(1.65367987605646,-0.803097400934551,
3.55557647058823));
#19112=CARTESIAN_POINT('Ctrl Pts',(1.57181488059719,0.953425691385454,3.66668823529412));
#19113=CARTESIAN_POINT('Ctrl Pts',(0.05186921357973,1.83764309716413,3.7778));
#19114=CARTESIAN_POINT('Ctrl Pts',(-1.5155324957619,1.04056898961853,3.88891176470588));
#19115=CARTESIAN_POINT('Ctrl Pts',(-1.69634726272219,-0.708539718097244,
4.00002352941176));
#19116=CARTESIAN_POINT('Ctrl Pts',(-0.325144523748834,-1.80939315974833,
4.11113529411765));
#19117=CARTESIAN_POINT('Ctrl Pts',(1.34353857429153,-1.25480144535206,4.22224705882353));
#19118=CARTESIAN_POINT('Ctrl Pts',(1.7829949491126,0.447829855308947,4.33335882352941));
#19119=CARTESIAN_POINT('Ctrl Pts',(0.591158348240881,1.74073386109778,4.44447058823529));
#19120=CARTESIAN_POINT('Ctrl Pts',(-1.14153926936423,1.44101029294259,4.55558235294118));
#19121=CARTESIAN_POINT('Ctrl Pts',(-1.82982282818684,-0.177118562870956,
4.66669411764705));
#19122=CARTESIAN_POINT('Ctrl Pts',(-0.843969773291502,-1.63319857630279,
4.77780588235294));
#19123=CARTESIAN_POINT('Ctrl Pts',(0.914045851976043,-1.59503691128215,
4.88891764705882));
#19124=CARTESIAN_POINT('Ctrl Pts',(1.83578508816481,-0.0975483364234787,
5.0000294117647));
#19125=CARTESIAN_POINT('Ctrl Pts',(1.07793273566426,1.48918890180207,5.11114117647059));
#19126=CARTESIAN_POINT('Ctrl Pts',(-0.666138955726334,1.7134414082573,5.22225294117646));
#19127=CARTESIAN_POINT('Ctrl Pts',(-1.8007485732889,0.370036678811588,5.33336470588236));
#19128=CARTESIAN_POINT('Ctrl Pts',(-1.28782211675415,-1.31192102028485,
5.44447647058823));
#19129=CARTESIAN_POINT('Ctrl Pts',(0.403355110511087,-1.79357944420943,
5.55558823529412));
#19130=CARTESIAN_POINT('Ctrl Pts',(1.72549575760574,-0.634260954463495,
5.6667));
#19131=CARTESIAN_POINT('Ctrl Pts',(1.46895043569095,1.10535387335637,5.77781176470588));
#19132=CARTESIAN_POINT('Ctrl Pts',(-0.131563094636045,1.83366128824048,
5.88892352941177));
#19133=CARTESIAN_POINT('Ctrl Pts',(-1.61170726989826,0.884320215792288,
6.00003529411764));
#19134=CARTESIAN_POINT('Ctrl Pts',(-1.6172725353172,-0.874100746094603,
6.11114705882353));
#19135=CARTESIAN_POINT('Ctrl Pts',(-0.143167133221453,-1.83279178845155,
6.2222588235294));
#19136=CARTESIAN_POINT('Ctrl Pts',(1.46192436006299,-1.11462986392232,6.3333705882353));
#19137=CARTESIAN_POINT('Ctrl Pts',(1.72947592303562,0.623326238098233,6.44448235294117));
#19138=CARTESIAN_POINT('Ctrl Pts',(0.414699995127109,1.79099036343795,6.55559411764706));
#19139=CARTESIAN_POINT('Ctrl Pts',(-1.27949214532916,1.32004637014752,6.66670588235293));
#19140=CARTESIAN_POINT('Ctrl Pts',(-1.80305474864053,-0.358630922043501,
6.77781764705883));
#19141=CARTESIAN_POINT('Ctrl Pts',(-0.676971321141057,-1.70919056845102,
6.8889294117647));
#19142=CARTESIAN_POINT('Ctrl Pts',(1.06848490487467,-1.49598214718639,7.00004117647059));
#19143=CARTESIAN_POINT('Ctrl Pts',(1.83636576494725,0.0859262661083765,
7.11115294117646));
#19144=CARTESIAN_POINT('Ctrl Pts',(0.924123786330422,1.58921924510457,7.22226470588235));
#19145=CARTESIAN_POINT('Ctrl Pts',(-0.833615098607335,1.63850800634715,
7.33337647058823));
#19146=CARTESIAN_POINT('Ctrl Pts',(-1.82866500741913,0.188697383424353,
7.44448823529411));
#19147=CARTESIAN_POINT('Ctrl Pts',(-1.15063775952351,-1.4337557146759,7.5556));
#19148=CARTESIAN_POINT('Ctrl Pts',(0.580128192863429,-1.74444092308354,
7.66671176470588));
#19149=CARTESIAN_POINT('Ctrl Pts',(1.7801242767762,-0.459106790715335,7.77782352941176));
#19150=CARTESIAN_POINT('Ctrl Pts',(1.35145482596167,1.2462718876643,7.88893529411764));
#19151=CARTESIAN_POINT('Ctrl Pts',(-0.313685993055972,1.81141522451351,
8.00004705882353));
#19152=CARTESIAN_POINT('Ctrl Pts',(-1.69182638778816,0.719262612778256,
8.1111588235294));
#19153=CARTESIAN_POINT('Ctrl Pts',(-1.52209249852947,-1.03095436009227,
8.2222705882353));
#19154=CARTESIAN_POINT('Ctrl Pts',(0.0402435134914415,-1.83793611758998,
8.33338235294118));
#19155=CARTESIAN_POINT('Ctrl Pts',(1.56573467327064,-0.963352952631984,
8.44449411764705));
#19156=CARTESIAN_POINT('Ctrl Pts',(1.65875634765081,0.792608392434986,8.55560588235294));
#19157=CARTESIAN_POINT('Ctrl Pts',(0.234061123673802,1.82341787389281,8.66671764705882));
#19158=CARTESIAN_POINT('Ctrl Pts',(-1.40460554046006,1.18591401264663,8.7778294117647));
#19159=CARTESIAN_POINT('Ctrl Pts',(-1.75850778925809,-0.536533168193233,
8.88894117647058));
#19160=CARTESIAN_POINT('Ctrl Pts',(-0.502885372776985,-1.76823019847661,
9.00005294117646));
#19161=CARTESIAN_POINT('Ctrl Pts',(1.21162302759592,-1.38188780683742,9.11116470588235));
#19162=CARTESIAN_POINT('Ctrl Pts',(1.81992793219366,0.268272986849182,9.22227647058824));
#19163=CARTESIAN_POINT('Ctrl Pts',(0.758516013178858,1.6740067592164,9.33338823529411));
#19164=CARTESIAN_POINT('Ctrl Pts',(-0.404795980777633,1.58843718658925,
9.40746274509804));
#19165=CARTESIAN_POINT('Ctrl Pts',(-0.840025297123196,1.30917445368946,
9.4445));
#19166=CARTESIAN_POINT('',(0.903606778650208,-1.26612599672284,0.));
#19167=CARTESIAN_POINT('Ctrl Pts',(0.903606778650207,-1.26612599672284,
-2.22044604925031E-15));
#19168=CARTESIAN_POINT('Ctrl Pts',(1.32452482391764,-0.965725878611127,
0.0370372549019586));
#19169=CARTESIAN_POINT('Ctrl Pts',(1.83597900638904,0.0826211852351528,
0.11111176470588));
#19170=CARTESIAN_POINT('Ctrl Pts',(0.924931235602245,1.59016045833715,0.222223529411763));
#19171=CARTESIAN_POINT('Ctrl Pts',(-0.83312512660499,1.63815347116992,0.333335294117645));
#19172=CARTESIAN_POINT('Ctrl Pts',(-1.53106292762084,0.622574687744289,
0.411242042445823));
#19173=CARTESIAN_POINT('Ctrl Pts',(-1.55772933110463,0.0543333176694591,
0.452111535872041));
#19174=CARTESIAN_POINT('Ctrl Pts',(-1.55735939632673,0.00101326450419686,
0.455943774396298));
#19175=CARTESIAN_POINT('Ctrl Pts',(0.863568020353686,1.756414520678,-8.67361737988404E-17));
#19176=CARTESIAN_POINT('Ctrl Pts',(0.902604744553569,1.73244180767701,-8.9279167384606E-17));
#19177=CARTESIAN_POINT('Ctrl Pts',(0.940679665251258,1.70703474391515,8.97961926050354E-17));
#19178=CARTESIAN_POINT('Ctrl Pts',(0.977702286264215,1.68018861076749,5.72458747072346E-17));
#19179=CARTESIAN_POINT('Ctrl Pts',(1.03586153234927,1.63801572236987,1.46490398407746E-17));
#19180=CARTESIAN_POINT('Ctrl Pts',(1.09142617933376,1.59229270785348,-2.67869138917656E-16));
#19181=CARTESIAN_POINT('Ctrl Pts',(1.14423485590453,1.54336034436958,-3.57353036051222E-16));
#19182=CARTESIAN_POINT('Ctrl Pts',(1.16947315095921,1.51997461483563,-4.00119133313148E-16));
#19183=CARTESIAN_POINT('Ctrl Pts',(1.19408133665882,1.49585539554391,8.18581218658372E-17));
#19184=CARTESIAN_POINT('Ctrl Pts',(1.21803815377257,1.47103794919798,5.55111512312578E-17));
#19185=CARTESIAN_POINT('Ctrl Pts',(1.23019217561359,1.45844730397601,4.21445318253017E-17));
#19186=CARTESIAN_POINT('Ctrl Pts',(1.24217850624866,1.44567693083781,1.93655380221213E-16));
#19187=CARTESIAN_POINT('Ctrl Pts',(1.25399412029808,1.43273135759888,2.04697370165263E-16));
#19188=CARTESIAN_POINT('Ctrl Pts',(1.26387705342325,1.42190329279817,2.13933220941147E-16));
#19189=CARTESIAN_POINT('Ctrl Pts',(1.27363384828941,1.41095997328553,2.33605914868334E-16));
#19190=CARTESIAN_POINT('Ctrl Pts',(1.28326192166555,1.39990597410978,2.08166817117217E-16));
#19191=CARTESIAN_POINT('Ctrl Pts',(1.33014969679031,1.34607407988414,8.42809005758918E-17));
#19192=CARTESIAN_POINT('Ctrl Pts',(1.37399942421539,1.28960720074626,-1.13965484205857E-16));
#19193=CARTESIAN_POINT('Ctrl Pts',(1.4146477049008,1.230839634391,-1.87350135405495E-16));
#19194=CARTESIAN_POINT('Ctrl Pts',(1.44368896684187,1.18885300520561,-2.39779976028666E-16));
#19195=CARTESIAN_POINT('Ctrl Pts',(1.47109515917518,1.14569133662427,-8.7819322856054E-17));
#19196=CARTESIAN_POINT('Ctrl Pts',(1.49679111505729,1.10147172806437,-6.24500451351651E-17));
#19197=CARTESIAN_POINT('Ctrl Pts',(1.51163881269315,1.07592064989137,-4.77911094423959E-17));
#19198=CARTESIAN_POINT('Ctrl Pts',(1.52591525031524,1.05001629664473,1.5220027212751E-16));
#19199=CARTESIAN_POINT('Ctrl Pts',(1.53960379146143,1.02378110502453,1.66533453693773E-16));
#19200=CARTESIAN_POINT('Ctrl Pts',(1.54537176342799,1.01272632218197,1.72573059272106E-16));
#19201=CARTESIAN_POINT('Ctrl Pts',(1.55103093390346,1.00162120437101,-1.75133660485687E-16));
#19202=CARTESIAN_POINT('Ctrl Pts',(1.55657976538519,0.990469147617543,-1.87350135405495E-16));
#19203=CARTESIAN_POINT('Ctrl Pts',(1.58759368815465,0.928137280446804,-2.55631324143141E-16));
#19204=CARTESIAN_POINT('Ctrl Pts',(1.61517308010414,0.864324080823349,1.42069026423598E-16));
#19205=CARTESIAN_POINT('Ctrl Pts',(1.63916386047712,0.799337824232817,2.77555756156289E-17));
#19206=CARTESIAN_POINT('Ctrl Pts',(1.66256346318323,0.735952950463245,-8.37409781139008E-17));
#19207=CARTESIAN_POINT('Ctrl Pts',(1.68254922594952,0.671451147944667,-8.96615244715113E-17));
#19208=CARTESIAN_POINT('Ctrl Pts',(1.69892983273053,0.606113461272593,-9.71445146547012E-17));
#19209=CARTESIAN_POINT('Ctrl Pts',(1.70969890177119,0.563158638650024,-1.02064041689972E-16));
#19210=CARTESIAN_POINT('Ctrl Pts',(1.71890879491296,0.519842467826019,-3.45159500757614E-16));
#19211=CARTESIAN_POINT('Ctrl Pts',(1.72649301018808,0.476246530743055,-3.05311331771918E-16));
#19212=CARTESIAN_POINT('Ctrl Pts',(1.73286946004292,0.43959312671897,-2.71808874084789E-16));
#19213=CARTESIAN_POINT('Ctrl Pts',(1.7380966173026,0.40274196097511,-2.63721634519194E-16));
#19214=CARTESIAN_POINT('Ctrl Pts',(1.74212938372161,0.365743253928757,-2.91433543964104E-16));
#19215=CARTESIAN_POINT('Ctrl Pts',(1.74338441815136,0.3542289120664,-3.00057748010143E-16));
#19216=CARTESIAN_POINT('Ctrl Pts',(1.74452367514155,0.342699905808242,-2.95319042101862E-16));
#19217=CARTESIAN_POINT('Ctrl Pts',(1.74554463432397,0.331172964307001,-2.77555756156289E-16));
#19218=CARTESIAN_POINT('Ctrl Pts',(1.75129363197339,0.266265022112653,-1.77531101983038E-16));
#19219=CARTESIAN_POINT('Ctrl Pts',(1.75330947147495,0.201304509751005,-1.61672294252907E-16));
#19220=CARTESIAN_POINT('Ctrl Pts',(1.75142501653378,0.136551819838445,-1.94289029309402E-16));
#19221=CARTESIAN_POINT('Ctrl Pts',(1.75088238549665,0.117906205917838,-2.03681056884401E-16));
#19222=CARTESIAN_POINT('Ctrl Pts',(1.75001603328345,0.0992778655205717,
5.11497906607206E-18));
#19223=CARTESIAN_POINT('Ctrl Pts',(1.74882116957219,0.0806731627252344,
-1.38777878078145E-17));
#19224=CARTESIAN_POINT('Ctrl Pts',(1.74442035560002,0.0121500037758971,
-8.61363537235156E-17));
#19225=CARTESIAN_POINT('Ctrl Pts',(1.73556731065817,-0.0560546348769042,
-8.94984743174132E-17));
#19226=CARTESIAN_POINT('Ctrl Pts',(1.72245500570668,-0.123603583729898,
-1.11022302462516E-16));
#19227=CARTESIAN_POINT('Ctrl Pts',(1.71065372503254,-0.184398700042928,
-1.30394086299314E-16));
#19228=CARTESIAN_POINT('Ctrl Pts',(1.69540112401956,-0.244662986427059,
-2.83658263324553E-17));
#19229=CARTESIAN_POINT('Ctrl Pts',(1.67680526621061,-0.304125446889571,
0.));
#19230=CARTESIAN_POINT('Ctrl Pts',(1.67349606673433,-0.31470700462369,5.04780035468084E-18));
#19231=CARTESIAN_POINT('Ctrl Pts',(1.67008251071857,-0.325257870756687,
-2.59895781250022E-16));
#19232=CARTESIAN_POINT('Ctrl Pts',(1.66656792507904,-0.33576950432459,-2.4980018054066E-16));
#19233=CARTESIAN_POINT('Ctrl Pts',(1.64601555867501,-0.397238754685905,
-1.90763780199754E-16));
#19234=CARTESIAN_POINT('Ctrl Pts',(1.62198854159901,-0.457444427764366,
-5.62956498032537E-16));
#19235=CARTESIAN_POINT('Ctrl Pts',(1.59467348808245,-0.516112566668481,
-4.9960036108132E-16));
#19236=CARTESIAN_POINT('Ctrl Pts',(1.5674666304738,-0.574548318967516,-4.36495180063804E-16));
#19237=CARTESIAN_POINT('Ctrl Pts',(1.53699697643864,-0.631459529320744,
-5.34526979994394E-16));
#19238=CARTESIAN_POINT('Ctrl Pts',(1.50340933089056,-0.686542989409802,
-5.27355936696949E-16));
#19239=CARTESIAN_POINT('Ctrl Pts',(1.47050931920745,-0.740498735664251,
-5.20331704887418E-16));
#19240=CARTESIAN_POINT('Ctrl Pts',(1.43461693006704,-0.792701424833635,
-2.68404534867939E-16));
#19241=CARTESIAN_POINT('Ctrl Pts',(1.39584139349689,-0.842824299455657,
-2.22044604925031E-16));
#19242=CARTESIAN_POINT('Ctrl Pts',(1.38890909242928,-0.851785280733763,
-2.13756363929169E-16));
#19243=CARTESIAN_POINT('Ctrl Pts',(1.38188458496569,-0.860679662653787,
-1.66156715466689E-16));
#19244=CARTESIAN_POINT('Ctrl Pts',(1.37476842993966,-0.869505410466454,
-1.66533453693773E-16));
#19245=CARTESIAN_POINT('Ctrl Pts',(1.36798353599758,-0.877920314673783,
-1.6689265454105E-16));
#19246=CARTESIAN_POINT('Ctrl Pts',(1.36111848029899,-0.886268835999708,
-1.80781753969063E-16));
#19247=CARTESIAN_POINT('Ctrl Pts',(1.35417907408573,-0.894543489490856,
-1.66533453693773E-16));
#19248=CARTESIAN_POINT('Ctrl Pts',(1.31430606770251,-0.942088668621772,
-8.46644075005493E-17));
#19249=CARTESIAN_POINT('Ctrl Pts',(1.27193077516495,-0.987260711017392,
3.92232772703659E-16));
#19250=CARTESIAN_POINT('Ctrl Pts',(1.22719194772877,-1.02979240857164,3.33066907387547E-16));
#19251=CARTESIAN_POINT('Ctrl Pts',(1.18325774198238,-1.07155917936502,2.74965132063436E-16));
#19252=CARTESIAN_POINT('Ctrl Pts',(1.13704354519755,-1.11078025986631,2.70799735769765E-17));
#19253=CARTESIAN_POINT('Ctrl Pts',(1.08865738848829,-1.14715869099291,2.77555756156289E-17));
#19254=CARTESIAN_POINT('Ctrl Pts',(1.04181551274958,-1.18237607683823,2.84096153016807E-17));
#19255=CARTESIAN_POINT('Ctrl Pts',(0.992937497203575,-1.21492966574416,
-2.26622882727394E-16));
#19256=CARTESIAN_POINT('Ctrl Pts',(0.942108816666581,-1.24450267784172,
-2.22044604925031E-16));
#19257=CARTESIAN_POINT('Ctrl Pts',(0.929396434173388,-1.25189896350738,
-2.20899565983063E-16));
#19258=CARTESIAN_POINT('Ctrl Pts',(0.916561996392962,-1.25910856034592,
-5.43661122892894E-17));
#19259=CARTESIAN_POINT('Ctrl Pts',(0.903606778650232,-1.26612599672282,
-5.55111512312578E-17));
#19260=CARTESIAN_POINT('Ctrl Pts',(1.57638112755711,1.1485113017068,9.04599999999999));
#19261=CARTESIAN_POINT('Ctrl Pts',(1.76277867682249,0.89337775104729,9.02806746277205));
#19262=CARTESIAN_POINT('Ctrl Pts',(1.89066037358035,0.595600609460199,9.01013492554411));
#19263=CARTESIAN_POINT('Ctrl Pts',(1.93659149294971,0.285826861476621,8.99220238831616));
#19264=CARTESIAN_POINT('Ctrl Pts',(2.03145607091723,-0.35396934360954,8.95516513341421));
#19265=CARTESIAN_POINT('Ctrl Pts',(1.77674102032598,-1.04493991917229,8.91812787851224));
#19266=CARTESIAN_POINT('Ctrl Pts',(1.29042609501658,-1.47131163503284,8.88109062361028));
#19267=CARTESIAN_POINT('Ctrl Pts',(0.804111169707157,-1.8976833508934,8.84405336870832));
#19268=CARTESIAN_POINT('Ctrl Pts',(0.086196369679569,-2.05945620705174,
8.80701611380637));
#19269=CARTESIAN_POINT('Ctrl Pts',(-0.535643940631454,-1.88246885422725,
8.7699788589044));
#19270=CARTESIAN_POINT('Ctrl Pts',(-1.15748425094246,-1.70548150140276,
8.73294160400244));
#19271=CARTESIAN_POINT('Ctrl Pts',(-1.68325007153691,-1.18973393959546,
8.69590434910048));
#19272=CARTESIAN_POINT('Ctrl Pts',(-1.87203837193898,-0.571240658920998,
8.65886709419851));
#19273=CARTESIAN_POINT('Ctrl Pts',(-1.92810375324022,-0.387563696209775,
8.64786796017375));
#19274=CARTESIAN_POINT('Ctrl Pts',(-1.95444971403581,-0.194825169918805,
8.63686882614899));
#19275=CARTESIAN_POINT('Ctrl Pts',(-1.95285709583883,-0.00166548583676096,
8.62586969212423));
#19276=CARTESIAN_POINT('Origin',(0.,0.,-1.2940562256037));
#19277=CARTESIAN_POINT('',(-0.903606778650184,-1.26612599672285,-1.38777878078145E-16));
#19278=CARTESIAN_POINT('Ctrl Pts',(-0.905550660636142,-1.26792405592273,
1.1310939164455E-15));
#19279=CARTESIAN_POINT('Ctrl Pts',(-0.51353745480643,-1.54485763355445,
0.0345106401883014));
#19280=CARTESIAN_POINT('Ctrl Pts',(0.588170214887261,-1.72164661131011,
0.106088614025153));
#19281=CARTESIAN_POINT('Ctrl Pts',(1.77543639638611,-0.478750755853424,
0.214733921510558));
#19282=CARTESIAN_POINT('Ctrl Pts',(1.36425885975684,1.23323526260274,0.325935922456214));
#19283=CARTESIAN_POINT('Ctrl Pts',(-0.297175317740204,1.81462004446968,
0.43713792340187));
#19284=CARTESIAN_POINT('Ctrl Pts',(-1.41354004632119,0.945824564565656,
0.526511357784366));
#19285=CARTESIAN_POINT('Ctrl Pts',(-1.55416372641,0.214215408672241,0.578817458518311));
#19286=CARTESIAN_POINT('Ctrl Pts',(-1.55326674879324,0.000737490386717929,
0.594056225603704));
#19287=CARTESIAN_POINT('Origin',(0.,0.,0.));
#19288=CARTESIAN_POINT('Ctrl Pts',(-0.685825729128738,1.39614588036675,
-0.230074082272066));
#19289=CARTESIAN_POINT('Ctrl Pts',(-1.1503452556824,1.16796095537201,-0.193006748623514));
#19290=CARTESIAN_POINT('Ctrl Pts',(-1.82566639114231,0.215444531932564,
-0.11887208132641));
#19291=CARTESIAN_POINT('Ctrl Pts',(-1.16908877997113,-1.42098933913104,
-0.00767008038075383));
#19292=CARTESIAN_POINT('Ctrl Pts',(0.560230897929427,-1.75089503242436,
0.103531920564902));
#19293=CARTESIAN_POINT('Ctrl Pts',(1.77543639638611,-0.478750755853424,
0.214733921510558));
#19294=CARTESIAN_POINT('Ctrl Pts',(1.36425885975684,1.23323526260274,0.325935922456214));
#19295=CARTESIAN_POINT('Ctrl Pts',(-0.297175317740204,1.81462004446968,
0.43713792340187));
#19296=CARTESIAN_POINT('Ctrl Pts',(-1.68620095450898,0.733629966765004,
0.548339924347525));
#19297=CARTESIAN_POINT('Ctrl Pts',(-1.53025640912295,-1.01973871733877,
0.659541925293182));
#19298=CARTESIAN_POINT('Ctrl Pts',(0.0278603330084876,-1.83865390028585,
0.770743926238836));
#19299=CARTESIAN_POINT('Ctrl Pts',(1.5604328654528,-0.972896783194139,0.881945927184494));
#19300=CARTESIAN_POINT('Ctrl Pts',(1.66322297628929,0.784329206349798,0.993147928130148));
#19301=CARTESIAN_POINT('Ctrl Pts',(0.242033178606095,1.82287837028977,1.10434992907581));
#19302=CARTESIAN_POINT('Ctrl Pts',(-1.40092403541303,1.19117010090687,1.21555193002146));
#19303=CARTESIAN_POINT('Ctrl Pts',(-1.76024597462735,-0.531985223933843,
1.32675393096712));
#19304=CARTESIAN_POINT('Ctrl Pts',(-0.506691785521986,-1.76769208329225,
1.43795593191277));
#19305=CARTESIAN_POINT('Ctrl Pts',(1.21113283005724,-1.38370173748454,1.54915793285843));
#19306=CARTESIAN_POINT('Ctrl Pts',(1.81922269924897,0.268145221691032,1.66035993380409));
#19307=CARTESIAN_POINT('Ctrl Pts',(0.760397896971566,1.67429621989364,1.77156193474974));
#19308=CARTESIAN_POINT('Ctrl Pts',(-0.99516307107971,1.54632579451077,1.8827639356954));
#19309=CARTESIAN_POINT('Ctrl Pts',(-1.83887757709731,0.00149027413755925,
1.99396593664105));
#19310=CARTESIAN_POINT('Ctrl Pts',(-0.997668151382599,-1.54471071329041,
2.10516793758671));
#19311=CARTESIAN_POINT('Ctrl Pts',(0.757683106401647,-1.67552656471375,
2.21636993853236));
#19312=CARTESIAN_POINT('Ctrl Pts',(1.81878565659978,-0.271093501731151,
2.32757193947802));
#19313=CARTESIAN_POINT('Ctrl Pts',(1.2133740808,1.38173669240563,2.43877394042368));
#19314=CARTESIAN_POINT('Ctrl Pts',(-0.50382603046139,1.76851131819754,2.54997594136933));
#19315=CARTESIAN_POINT('Ctrl Pts',(-1.75938120199744,0.534837111883675,
2.66117794231499));
#19316=CARTESIAN_POINT('Ctrl Pts',(-1.40285327152777,-1.18889681987293,
2.77237994326064));
#19317=CARTESIAN_POINT('Ctrl Pts',(0.239078896742882,-1.82327020255007,
2.88358194420631));
#19318=CARTESIAN_POINT('Ctrl Pts',(1.66194822130476,-0.787020368122459,
2.99478394515195));
#19319=CARTESIAN_POINT('Ctrl Pts',(1.56201018579718,0.970359278599158,3.10598594609762));
#19320=CARTESIAN_POINT('Ctrl Pts',(0.0308358597469676,1.83861961806662,
3.21718794704326));
#19321=CARTESIAN_POINT('Ctrl Pts',(-1.52859270045602,1.02219240178121,3.32838994798893));
#19322=CARTESIAN_POINT('Ctrl Pts',(-1.68740469215855,-0.730847696189792,
3.43959194893457));
#19323=CARTESIAN_POINT('Ctrl Pts',(-0.300084107876245,-1.81422779119842,
3.55079394988024));
#19324=CARTESIAN_POINT('Ctrl Pts',(1.36219708122283,-1.23527003608861,3.66199595082589));
#19325=CARTESIAN_POINT('Ctrl Pts',(1.77632642388981,0.475539047756765,3.77319795177155));
#19326=CARTESIAN_POINT('Ctrl Pts',(0.562846122986205,1.75062194433623,3.8843999527172));
#19327=CARTESIAN_POINT('Ctrl Pts',(-1.16635795779188,1.42164765833408,3.99560195366286));
#19328=CARTESIAN_POINT('Ctrl Pts',(-1.82685336294205,-0.209951757455398,
4.10680395460851));
#19329=CARTESIAN_POINT('Ctrl Pts',(-0.813442378520323,-1.64917689984389,
4.21800595555418));
#19330=CARTESIAN_POINT('Ctrl Pts',(0.945308337362415,-1.57729676898942,
4.32920795649982));
#19331=CARTESIAN_POINT('Ctrl Pts',(1.83789338383513,-0.0601735806349488,
4.44040995744549));
#19332=CARTESIAN_POINT('Ctrl Pts',(1.04645630737228,1.51208536363268,4.55161195839114));
#19333=CARTESIAN_POINT('Ctrl Pts',(-0.703826144888774,1.69885305660096,
4.66281395933679));
#19334=CARTESIAN_POINT('Ctrl Pts',(-1.80920785964355,0.328998283818298,
4.77401596028245));
#19335=CARTESIAN_POINT('Ctrl Pts',(-1.25685137944873,-1.34231053043966,
4.88521796122811));
#19336=CARTESIAN_POINT('Ctrl Pts',(0.447130949584586,-1.78368911643119,
4.99641996217376));
#19337=CARTESIAN_POINT('Ctrl Pts',(1.74141681985029,-0.590711782254083,
5.10762196311942));
#19338=CARTESIAN_POINT('Ctrl Pts',(1.44007996484097,1.14352203521175,5.21882396406507));
#19339=CARTESIAN_POINT('Ctrl Pts',(-0.18077114541208,1.82997124106871,5.33002596501073));
#19340=CARTESIAN_POINT('Ctrl Pts',(-1.63598554858516,0.839657212778587,
5.44122796595639));
#19341=CARTESIAN_POINT('Ctrl Pts',(-1.5921816295577,-0.920016634985102,
5.55242996690203));
#19342=CARTESIAN_POINT('Ctrl Pts',(-0.089495975882287,-1.83669905549533,
5.66363196784771));
#19343=CARTESIAN_POINT('Ctrl Pts',(1.49519291292304,-1.07045369039924,5.77483396879335));
#19344=CARTESIAN_POINT('Ctrl Pts',(1.70986873918469,0.676625335695913,5.88603596973901));
#19345=CARTESIAN_POINT('Ctrl Pts',(0.357828666998206,1.80372713991337,5.99723797068467));
#19346=CARTESIAN_POINT('Ctrl Pts',(-1.32208210581628,1.27811261459153,6.10843997163031));
#19347=CARTESIAN_POINT('Ctrl Pts',(-1.79059752017374,-0.418608971338806,
6.21964197257599));
#19348=CARTESIAN_POINT('Ctrl Pts',(-0.618426992791356,-1.73176817298442,
6.33084397352162));
#19349=CARTESIAN_POINT('Ctrl Pts',(1.12039486833334,-1.45814549642773,6.4420459744673));
#19350=CARTESIAN_POINT('Ctrl Pts',(1.83262304280178,0.151544492417154,6.55324797541294));
#19351=CARTESIAN_POINT('Ctrl Pts',(0.865658194202354,1.62237752769619,6.6644499763586));
#19352=CARTESIAN_POINT('Ctrl Pts',(-0.894490612933678,1.60666097558597,
6.77565197730426));
#19353=CARTESIAN_POINT('Ctrl Pts',(-1.83503693743053,0.11879557904028,6.8868539782499));
#19354=CARTESIAN_POINT('Ctrl Pts',(-1.09417843856274,-1.47791965389608,
6.99805597919557));
#19355=CARTESIAN_POINT('Ctrl Pts',(0.649252195647424,-1.72044892818251,
7.10925798014122));
#19356=CARTESIAN_POINT('Ctrl Pts',(1.79778702933405,-0.386567926277561,
7.22045998108688));
#19357=CARTESIAN_POINT('Ctrl Pts',(1.29904832373936,1.30151698160267,7.33166198203254));
#19358=CARTESIAN_POINT('Ctrl Pts',(-0.389980372076409,1.79704983321667,
7.44286398297819));
#19359=CARTESIAN_POINT('Ctrl Pts',(-1.72167847110372,0.645984776536109,
7.55406598392385));
#19360=CARTESIAN_POINT('Ctrl Pts',(-1.47583963303223,-1.09698250119657,
7.6652679848695));
#19361=CARTESIAN_POINT('Ctrl Pts',(0.122279206149944,-1.83480779990519,
7.77646998581516));
#19362=CARTESIAN_POINT('Ctrl Pts',(1.6083563717128,-0.891439258304551,7.88767198676082));
#19363=CARTESIAN_POINT('Ctrl Pts',(1.6207309884821,0.868737834600438,7.99887398770647));
#19364=CARTESIAN_POINT('Ctrl Pts',(0.148065176955119,1.83290543012718,8.11007598865213));
#19365=CARTESIAN_POINT('Ctrl Pts',(-1.46027046044108,1.11762836182387,8.22127798959778));
#19366=CARTESIAN_POINT('Ctrl Pts',(-1.73059002514951,-0.621721033251858,
8.33247999054344));
#19367=CARTESIAN_POINT('Ctrl Pts',(-0.415210463238687,-1.79137506804378,
8.4436819914891));
#19368=CARTESIAN_POINT('Ctrl Pts',(1.28062367350908,-1.31967978545922,8.55488399243474));
#19369=CARTESIAN_POINT('Ctrl Pts',(1.80303816946195,0.361303122856545,8.66608599338042));
#19370=CARTESIAN_POINT('Ctrl Pts',(0.673390003682997,1.71105376251155,8.77728799432605));
#19371=CARTESIAN_POINT('Ctrl Pts',(-1.07331353684551,1.49334172277348,8.88848999527173));
#19372=CARTESIAN_POINT('Ctrl Pts',(-1.83648185490594,-0.0933331690448563,
8.99969199621736));
#19373=CARTESIAN_POINT('Ctrl Pts',(-0.917075781704608,-1.59325581253419,
9.11089399716304));
#19374=CARTESIAN_POINT('Ctrl Pts',(0.84291969341562,-1.63568507599433,9.22209599810868));
#19375=CARTESIAN_POINT('Ctrl Pts',(1.83002015964776,-0.174643446395858,
9.33329799905435));
#19376=CARTESIAN_POINT('Ctrl Pts',(1.37089695500413,0.898926325849287,9.40743266635145));
#19377=CARTESIAN_POINT('Ctrl Pts',(0.964986447796868,1.2199923793075,9.4445));
#19378=CARTESIAN_POINT('Ctrl Pts',(-0.744392439309333,1.51537102412035,
-0.153382721514711));
#19379=CARTESIAN_POINT('Ctrl Pts',(-1.24858003215071,1.26770004049271,-0.116315387866159));
#19380=CARTESIAN_POINT('Ctrl Pts',(-1.98157082848726,0.233842613144434,
-0.0421807205690546));
#19381=CARTESIAN_POINT('Ctrl Pts',(-1.26892417669641,-1.54233601257873,
0.0690212803766013));
#19382=CARTESIAN_POINT('Ctrl Pts',(0.60807232358566,-1.90041430177422,0.180223281322257));
#19383=CARTESIAN_POINT('Ctrl Pts',(1.92705139777042,-0.519634110874885,
0.291425282267913));
#19384=CARTESIAN_POINT('Ctrl Pts',(1.48076098246403,1.33854850639298,0.402627283213569));
#19385=CARTESIAN_POINT('Ctrl Pts',(-0.32255287353564,1.96958116902152,0.513829284159225));
#19386=CARTESIAN_POINT('Ctrl Pts',(-1.83019561439793,0.796278963176857,
0.62503128510488));
#19387=CARTESIAN_POINT('Ctrl Pts',(-1.6609340431175,-1.10682023000553,0.736233286050537));
#19388=CARTESIAN_POINT('Ctrl Pts',(0.0302394914149615,-1.99566741775375,
0.847435286996192));
#19389=CARTESIAN_POINT('Ctrl Pts',(1.69368744530556,-1.05597818640917,0.958637287941849));
#19390=CARTESIAN_POINT('Ctrl Pts',(1.80525541088723,0.85130771031001,1.0698392888875));
#19391=CARTESIAN_POINT('Ctrl Pts',(0.262701821416467,1.97854472206529,1.18104128983316));
#19392=CARTESIAN_POINT('Ctrl Pts',(-1.52055721405056,1.29289115206115,1.29224329077882));
#19393=CARTESIAN_POINT('Ctrl Pts',(-1.91056377616791,-0.577414584640491,
1.40344529172447));
#19394=CARTESIAN_POINT('Ctrl Pts',(-0.549961190114417,-1.91864575203584,
1.51464729267013));
#19395=CARTESIAN_POINT('Ctrl Pts',(1.31455861657342,-1.50186420236992,1.62584929361578));
#19396=CARTESIAN_POINT('Ctrl Pts',(1.97457687168029,0.291043726104147,1.73705129456144));
#19397=CARTESIAN_POINT('Ctrl Pts',(0.825332765061831,1.81727426417256,1.8482532955071));
#19398=CARTESIAN_POINT('Ctrl Pts',(-1.08014592414415,1.67837568824538,1.95945529645275));
#19399=CARTESIAN_POINT('Ctrl Pts',(-1.99591019564939,0.00161753744922554,
2.07065729739841));
#19400=CARTESIAN_POINT('Ctrl Pts',(-1.08286492805163,-1.67662268569932,
2.18185929834406));
#19401=CARTESIAN_POINT('Ctrl Pts',(0.822386142488863,-1.81860967540451,
2.29306129928972));
#19402=CARTESIAN_POINT('Ctrl Pts',(1.97410250737766,-0.294243777192403,
2.40426330023538));
#19403=CARTESIAN_POINT('Ctrl Pts',(1.31699126095619,1.49973135048419,2.51546530118103));
#19404=CARTESIAN_POINT('Ctrl Pts',(-0.546850711301162,1.91953494624891,
2.62666730212668));
#19405=CARTESIAN_POINT('Ctrl Pts',(-1.90962515549492,0.58051001214848,2.73786930307235));
#19406=CARTESIAN_POINT('Ctrl Pts',(-1.52265119903315,-1.29042374213144,
2.849071304018));
#19407=CARTESIAN_POINT('Ctrl Pts',(0.259495255973991,-1.97897001519685,
2.96027330496365));
#19408=CARTESIAN_POINT('Ctrl Pts',(1.80387179704459,-0.854228686283152,
3.07147530590931));
#19409=CARTESIAN_POINT('Ctrl Pts',(1.69539946235139,1.05322398930777,3.18267730685497));
#19410=CARTESIAN_POINT('Ctrl Pts',(0.0334691159580969,1.99563020797331,
3.29387930780062));
#19411=CARTESIAN_POINT('Ctrl Pts',(-1.65912826053996,1.10948344905644,3.40508130874628));
#19412=CARTESIAN_POINT('Ctrl Pts',(-1.83150214631588,-0.793259098082338,
3.51628330969193));
#19413=CARTESIAN_POINT('Ctrl Pts',(-0.325710062443639,-1.96915541892639,
3.62748531063759));
#19414=CARTESIAN_POINT('Ctrl Pts',(1.47852313648206,-1.34075704120622,3.73868731158324));
#19415=CARTESIAN_POINT('Ctrl Pts',(1.92801742998006,0.516148136052275,3.84988931252891));
#19416=CARTESIAN_POINT('Ctrl Pts',(0.610910878158188,1.90011789308111,3.96109131347456));
#19417=CARTESIAN_POINT('Ctrl Pts',(-1.26596015348029,1.54305054954723,4.07229331442022));
#19418=CARTESIAN_POINT('Ctrl Pts',(-1.98285916282043,-0.227880778208832,
4.18349531536587));
#19419=CARTESIAN_POINT('Ctrl Pts',(-0.882907028223612,-1.79000985700403,
4.29469731631152));
#19420=CARTESIAN_POINT('Ctrl Pts',(1.02603380022298,-1.71199145718021,4.40589931725719));
#19421=CARTESIAN_POINT('Ctrl Pts',(1.99484195631093,-0.0653121581305224,
4.51710131820284));
#19422=CARTESIAN_POINT('Ctrl Pts',(1.13581939287274,1.64121126471649,4.62830331914849));
#19423=CARTESIAN_POINT('Ctrl Pts',(-0.763930016899512,1.84392815422348,
4.73950532009415));
#19424=CARTESIAN_POINT('Ctrl Pts',(-1.96370680576333,0.357093390665327,
4.8507073210398));
#19425=CARTESIAN_POINT('Ctrl Pts',(-1.36418134295679,-1.45693835565774,
4.96190932198546));
#19426=CARTESIAN_POINT('Ctrl Pts',(0.485314102570633,-1.93600886632894,
5.07311132293112));
#19427=CARTESIAN_POINT('Ctrl Pts',(1.89012668864067,-0.64115615067331,5.18431332387677));
#19428=CARTESIAN_POINT('Ctrl Pts',(1.56305689958632,1.24117413657934,5.29551532482243));
#19429=CARTESIAN_POINT('Ctrl Pts',(-0.196208261333358,1.98624329497761,
5.40671732576808));
#19430=CARTESIAN_POINT('Ctrl Pts',(-1.77569201834004,0.911360502030131,
5.51791932671374));
#19431=CARTESIAN_POINT('Ctrl Pts',(-1.72814742391724,-0.998582289981674,
5.6291213276594));
#19432=CARTESIAN_POINT('Ctrl Pts',(-0.0971385659153217,-1.9935456372193,
5.74032332860505));
#19433=CARTESIAN_POINT('Ctrl Pts',(1.62287626785709,-1.16186605418883,5.8515253295507));
#19434=CARTESIAN_POINT('Ctrl Pts',(1.85588453101264,0.734406369934583,5.96272733049637));
#19435=CARTESIAN_POINT('Ctrl Pts',(0.388385770565944,1.95775805500079,6.07392933144201));
#19436=CARTESIAN_POINT('Ctrl Pts',(-1.43498250636653,1.38725820055848,6.18513133238768));
#19437=CARTESIAN_POINT('Ctrl Pts',(-1.94350721947498,-0.454356464123216,
6.29633333333333));
#19438=CARTESIAN_POINT('Ctrl Pts',(-0.671238126752017,-1.8796540868244,
6.40753533427899));
#19439=CARTESIAN_POINT('Ctrl Pts',(1.21607200430908,-1.58266515362831,6.51873733522465));
#19440=CARTESIAN_POINT('Ctrl Pts',(1.98912154972485,0.164485771797453,6.6299393361703));
#19441=CARTESIAN_POINT('Ctrl Pts',(0.939581860845384,1.76092192816482,6.74114133711596));
#19442=CARTESIAN_POINT('Ctrl Pts',(-0.970876450125151,1.7438632468323,6.85234333806161));
#19443=CARTESIAN_POINT('Ctrl Pts',(-1.99174158107482,0.128940235259636,
6.96354533900727));
#19444=CARTESIAN_POINT('Ctrl Pts',(-1.18761679874002,-1.60412794320875,
7.07474733995293));
#19445=CARTESIAN_POINT('Ctrl Pts',(0.704695675764305,-1.86736822484612,
7.18594934089858));
#19446=CARTESIAN_POINT('Ctrl Pts',(1.95131068329089,-0.419579244957874,
7.29715134184424));
#19447=CARTESIAN_POINT('Ctrl Pts',(1.4099817335776,1.4126612047182,7.40835334278989));
#19448=CARTESIAN_POINT('Ctrl Pts',(-0.423283099660761,1.95051053364244,
7.51955534373554));
#19449=CARTESIAN_POINT('Ctrl Pts',(-1.86870276570027,0.701149232434471,
7.63075734468121));
#19450=CARTESIAN_POINT('Ctrl Pts',(-1.60187029707667,-1.19066031684572,
7.74195934562685));
#19451=CARTESIAN_POINT('Ctrl Pts',(0.132721349865937,-1.99149287614267,
7.85316134657253));
#19452=CARTESIAN_POINT('Ctrl Pts',(1.7457034228491,-0.967564522299928,7.96436334751815));
#19453=CARTESIAN_POINT('Ctrl Pts',(1.75913478124116,0.942924489928461,8.07556534846384));
#19454=CARTESIAN_POINT('Ctrl Pts',(0.160709337035842,1.98942805177203,8.18676734940947));
#19455=CARTESIAN_POINT('Ctrl Pts',(-1.58497158087089,1.21306924946704,8.29796935035515));
#19456=CARTESIAN_POINT('Ctrl Pts',(-1.87837532998656,-0.674813464785299,
8.4091713513008));
#19457=CARTESIAN_POINT('Ctrl Pts',(-0.45066773734148,-1.94435116675061,
8.52037335224644));
#19458=CARTESIAN_POINT('Ctrl Pts',(1.38998369362979,-1.4323750376837,8.63157535319211));
#19459=CARTESIAN_POINT('Ctrl Pts',(1.95701024929279,0.392156930733598,8.74277735413776));
#19460=CARTESIAN_POINT('Ctrl Pts',(0.730894753810015,1.8571707504813,8.85397935508342));
#19461=CARTESIAN_POINT('Ctrl Pts',(-1.16497011981623,1.62086699364572,8.96518135602907));
#19462=CARTESIAN_POINT('Ctrl Pts',(-1.99330988858858,-0.101303439668302,
9.07638335697474));
#19463=CARTESIAN_POINT('Ctrl Pts',(-0.995390299867974,-1.72931333772327,
9.18758535792038));
#19464=CARTESIAN_POINT('Ctrl Pts',(0.914901585160197,-1.7753658866198,9.29878735886605));
#19465=CARTESIAN_POINT('Ctrl Pts',(1.98629639100309,-0.189557281901872,
9.40998935981169));
#19466=CARTESIAN_POINT('Ctrl Pts',(1.4879659438757,0.975690954768368,9.4841240271088));
#19467=CARTESIAN_POINT('Ctrl Pts',(1.04739234074599,1.3241747350675,9.52119136075735));
#19468=CARTESIAN_POINT('Ctrl Pts',(-0.802959149489929,1.63459616787395,
-0.0766913607573553));
#19469=CARTESIAN_POINT('Ctrl Pts',(-1.34681480861903,1.36743912561342,-0.0396240271088033));
#19470=CARTESIAN_POINT('Ctrl Pts',(-2.13747526583221,0.252240694356305,
0.0345106401883006));
#19471=CARTESIAN_POINT('Ctrl Pts',(-1.3687595734217,-1.66368268602643,0.145712641133957));
#19472=CARTESIAN_POINT('Ctrl Pts',(0.655913749241891,-2.04993357112408,
0.256914642079612));
#19473=CARTESIAN_POINT('Ctrl Pts',(2.07866639915472,-0.560517465896349,
0.368116643025269));
#19474=CARTESIAN_POINT('Ctrl Pts',(1.59726310517123,1.44386175018322,0.479318643970924));
#19475=CARTESIAN_POINT('Ctrl Pts',(-0.347930429331078,2.12454229357336,
0.590520644916581));
#19476=CARTESIAN_POINT('Ctrl Pts',(-1.97419027428688,0.858927959588711,
0.701722645862234));
#19477=CARTESIAN_POINT('Ctrl Pts',(-1.79161167711204,-1.19390174267229,
0.812924646807894));
#19478=CARTESIAN_POINT('Ctrl Pts',(0.0326186498214368,-2.15268093522164,
0.924126647753546));
#19479=CARTESIAN_POINT('Ctrl Pts',(1.82694202515831,-1.13905958962419,1.03532864869921));
#19480=CARTESIAN_POINT('Ctrl Pts',(1.94728784548518,0.918286214270224,1.14653064964486));
#19481=CARTESIAN_POINT('Ctrl Pts',(0.283370464226838,2.13421107384081,1.25773265059052));
#19482=CARTESIAN_POINT('Ctrl Pts',(-1.6401903926881,1.39461220321543,1.36893465153617));
#19483=CARTESIAN_POINT('Ctrl Pts',(-2.06088157770847,-0.622843945347137,
1.48013665248183));
#19484=CARTESIAN_POINT('Ctrl Pts',(-0.593230594706847,-2.06959942077943,
1.59133865342748));
#19485=CARTESIAN_POINT('Ctrl Pts',(1.4179844030896,-1.6200266672553,1.70254065437314));
#19486=CARTESIAN_POINT('Ctrl Pts',(2.1299310441116,0.313942230517263,1.81374265531879));
#19487=CARTESIAN_POINT('Ctrl Pts',(0.890267633152099,1.96025230845148,1.92494465626445));
#19488=CARTESIAN_POINT('Ctrl Pts',(-1.16512877720859,1.81042558198,2.03614665721011));
#19489=CARTESIAN_POINT('Ctrl Pts',(-2.15294281420147,0.00174480076089232,
2.14734865815576));
#19490=CARTESIAN_POINT('Ctrl Pts',(-1.16806170472066,-1.80853465810824,
2.25855065910142));
#19491=CARTESIAN_POINT('Ctrl Pts',(0.88708917857608,-1.96169278609528,2.36975266004707));
#19492=CARTESIAN_POINT('Ctrl Pts',(2.12941935815555,-0.317394052653655,
2.48095466099273));
#19493=CARTESIAN_POINT('Ctrl Pts',(1.42060844111238,1.61772600856275,2.59215666193839));
#19494=CARTESIAN_POINT('Ctrl Pts',(-0.589875392140936,2.07055857430028,
2.70335866288404));
#19495=CARTESIAN_POINT('Ctrl Pts',(-2.05986910899239,0.626182912413284,
2.8145606638297));
#19496=CARTESIAN_POINT('Ctrl Pts',(-1.64244912653854,-1.39195066438994,
2.92576266477535));
#19497=CARTESIAN_POINT('Ctrl Pts',(0.2799116152051,-2.13466982784364,3.03696466572101));
#19498=CARTESIAN_POINT('Ctrl Pts',(1.94579537278442,-0.921437004443841,
3.14816666666667));
#19499=CARTESIAN_POINT('Ctrl Pts',(1.8287887389056,1.13608870001637,3.25936866761232));
#19500=CARTESIAN_POINT('Ctrl Pts',(0.0361023721692252,2.15264079787999,
3.37057066855798));
#19501=CARTESIAN_POINT('Ctrl Pts',(-1.78966382062389,1.19677449633167,3.48177266950363));
#19502=CARTESIAN_POINT('Ctrl Pts',(-1.97559960047322,-0.855670499974885,
3.59297467044929));
#19503=CARTESIAN_POINT('Ctrl Pts',(-0.351336017011034,-2.12408304665435,
3.70417667139495));
#19504=CARTESIAN_POINT('Ctrl Pts',(1.59484919174131,-1.44624404632384,3.8153786723406));
#19505=CARTESIAN_POINT('Ctrl Pts',(2.0797084360703,0.556757224347788,3.92658067328626));
#19506=CARTESIAN_POINT('Ctrl Pts',(0.658975633330173,2.04961384182598,4.03778267423191));
#19507=CARTESIAN_POINT('Ctrl Pts',(-1.36556234916871,1.66445344076038,4.14898467517757));
#19508=CARTESIAN_POINT('Ctrl Pts',(-2.1388649626988,-0.245809798962268,
4.26018667612322));
#19509=CARTESIAN_POINT('Ctrl Pts',(-0.952371677926902,-1.93084281416416,
4.37138867706889));
#19510=CARTESIAN_POINT('Ctrl Pts',(1.10675926308356,-1.846686145371,4.48259067801454));
#19511=CARTESIAN_POINT('Ctrl Pts',(2.15179052878673,-0.0704507356260967,
4.59379267896019));
#19512=CARTESIAN_POINT('Ctrl Pts',(1.2251824783732,1.7703371658003,4.70499467990585));
#19513=CARTESIAN_POINT('Ctrl Pts',(-0.824033888910251,1.98900325184601,
4.8161966808515));
#19514=CARTESIAN_POINT('Ctrl Pts',(-2.11820575188311,0.385188497512356,
4.92739868179717));
#19515=CARTESIAN_POINT('Ctrl Pts',(-1.47151130646485,-1.57156618087582,
5.03860068274281));
#19516=CARTESIAN_POINT('Ctrl Pts',(0.523497255556681,-2.08832861622669,
5.14980268368848));
#19517=CARTESIAN_POINT('Ctrl Pts',(2.03883655743106,-0.691600519092537,
5.26100468463412));
#19518=CARTESIAN_POINT('Ctrl Pts',(1.68603383433167,1.33882623794692,5.37220668557979));
#19519=CARTESIAN_POINT('Ctrl Pts',(-0.211645377254637,2.14251534888651,
5.48340868652544));
#19520=CARTESIAN_POINT('Ctrl Pts',(-1.91539848809492,0.983063791281674,
5.5946106874711));
#19521=CARTESIAN_POINT('Ctrl Pts',(-1.86411321827678,-1.07714794497825,
5.70581268841674));
#19522=CARTESIAN_POINT('Ctrl Pts',(-0.104781155948357,-2.15039221894326,
5.81701468936241));
#19523=CARTESIAN_POINT('Ctrl Pts',(1.75055962279115,-1.25327841797843,5.92821669030807));
#19524=CARTESIAN_POINT('Ctrl Pts',(2.00190032284059,0.792187404173254,6.03941869125372));
#19525=CARTESIAN_POINT('Ctrl Pts',(0.418942874133682,2.11178897008822,6.15062069219938));
#19526=CARTESIAN_POINT('Ctrl Pts',(-1.54788290691678,1.49640378652543,6.26182269314503));
#19527=CARTESIAN_POINT('Ctrl Pts',(-2.09641691877623,-0.490103956907626,
6.37302469409069));
#19528=CARTESIAN_POINT('Ctrl Pts',(-0.724049260712674,-2.02754000066438,
6.48422669503635));
#19529=CARTESIAN_POINT('Ctrl Pts',(1.31174914028481,-1.70718481082889,6.59542869598199));
#19530=CARTESIAN_POINT('Ctrl Pts',(2.14562005664793,0.177427051177754,6.70663069692766));
#19531=CARTESIAN_POINT('Ctrl Pts',(1.01350552748841,1.89946632863346,6.81783269787331));
#19532=CARTESIAN_POINT('Ctrl Pts',(-1.04726228731662,1.88106551807864,6.92903469881897));
#19533=CARTESIAN_POINT('Ctrl Pts',(-2.14844622471911,0.13908489147899,7.04023669976463));
#19534=CARTESIAN_POINT('Ctrl Pts',(-1.28105515891731,-1.73033623252141,
7.15143870071027));
#19535=CARTESIAN_POINT('Ctrl Pts',(0.760139155881188,-2.01428752150974,
7.26264070165595));
#19536=CARTESIAN_POINT('Ctrl Pts',(2.10483433724774,-0.452590563638184,
7.37384270260158));
#19537=CARTESIAN_POINT('Ctrl Pts',(1.52091514341585,1.52380542783373,7.48504470354725));
#19538=CARTESIAN_POINT('Ctrl Pts',(-0.456585827245116,2.10397123406821,
7.59624670449291));
#19539=CARTESIAN_POINT('Ctrl Pts',(-2.01572706029682,0.756313688332832,
7.70744870543855));
#19540=CARTESIAN_POINT('Ctrl Pts',(-1.72790096112112,-1.28433813249488,
7.81865070638422));
#19541=CARTESIAN_POINT('Ctrl Pts',(0.143163493581931,-2.14817795238016,
7.92985270732987));
#19542=CARTESIAN_POINT('Ctrl Pts',(1.88305047398539,-1.0436897862953,8.04105470827553));
#19543=CARTESIAN_POINT('Ctrl Pts',(1.89753857400022,1.01711114525648,8.15225670922118));
#19544=CARTESIAN_POINT('Ctrl Pts',(0.173353497116561,2.14595067341688,8.26345871016684));
#19545=CARTESIAN_POINT('Ctrl Pts',(-1.7096727013007,1.30851013711022,8.3746607111125));
#19546=CARTESIAN_POINT('Ctrl Pts',(-2.02616063482361,-0.72790589631874,
8.48586271205815));
#19547=CARTESIAN_POINT('Ctrl Pts',(-0.486125011444274,-2.09732726545744,
8.59706471300382));
#19548=CARTESIAN_POINT('Ctrl Pts',(1.49934371375051,-1.54507028990818,8.70826671394946));
#19549=CARTESIAN_POINT('Ctrl Pts',(2.11098232912363,0.423010738610651,8.81946871489512));
#19550=CARTESIAN_POINT('Ctrl Pts',(0.788399503937036,2.00328773845105,8.93067071584077));
#19551=CARTESIAN_POINT('Ctrl Pts',(-1.25662670278695,1.74839226451795,9.04187271678643));
#19552=CARTESIAN_POINT('Ctrl Pts',(-2.15013792227122,-0.109273710291747,
9.15307471773208));
#19553=CARTESIAN_POINT('Ctrl Pts',(-1.07370481803134,-1.86537086291235,
9.26427671867775));
#19554=CARTESIAN_POINT('Ctrl Pts',(0.986883476904773,-1.91504669724527,
9.37547871962339));
#19555=CARTESIAN_POINT('Ctrl Pts',(2.14257262235841,-0.204471117407888,
9.48668072056906));
#19556=CARTESIAN_POINT('Ctrl Pts',(1.60503493274727,1.05245558368745,9.56081538786616));
#19557=CARTESIAN_POINT('Ctrl Pts',(1.12979823369512,1.42835709082749,9.59788272151471));
#19558=CARTESIAN_POINT('Ctrl Pts',(-0.861525859670525,1.75382131162755,
0.));
#19559=CARTESIAN_POINT('Ctrl Pts',(-1.44504958508734,1.46717821073413,0.037067333648552));
#19560=CARTESIAN_POINT('Ctrl Pts',(-2.29337970317716,0.270638775568176,
0.111202000945656));
#19561=CARTESIAN_POINT('Ctrl Pts',(-1.46859497014699,-1.78502935947413,
0.222404001891312));
#19562=CARTESIAN_POINT('Ctrl Pts',(0.703755174898128,-2.19945284047394,
0.333606002836967));
#19563=CARTESIAN_POINT('Ctrl Pts',(2.23028140053902,-0.601400820917812,
0.444808003782624));
#19564=CARTESIAN_POINT('Ctrl Pts',(1.71376522787844,1.54917499397346,0.556010004728279));
#19565=CARTESIAN_POINT('Ctrl Pts',(-0.373307985126514,2.27950341812521,
0.667212005673936));
#19566=CARTESIAN_POINT('Ctrl Pts',(-2.11818493417584,0.921576956000567,
0.778414006619591));
#19567=CARTESIAN_POINT('Ctrl Pts',(-1.92228931110658,-1.28098325533905,
0.889616007565248));
#19568=CARTESIAN_POINT('Ctrl Pts',(0.0349978082279097,-2.30969445268953,
1.0008180085109));
#19569=CARTESIAN_POINT('Ctrl Pts',(1.96019660501108,-1.22214099283922,1.11202000945656));
#19570=CARTESIAN_POINT('Ctrl Pts',(2.08932028008312,0.985264718230436,1.22322201040222));
#19571=CARTESIAN_POINT('Ctrl Pts',(0.304039107037209,2.28987742561633,1.33442401134787));
#19572=CARTESIAN_POINT('Ctrl Pts',(-1.75982357132563,1.49633325436971,1.44562601229353));
#19573=CARTESIAN_POINT('Ctrl Pts',(-2.21119937924903,-0.668273306053786,
1.55682801323918));
#19574=CARTESIAN_POINT('Ctrl Pts',(-0.636499999299278,-2.22055308952301,
1.66803001418484));
#19575=CARTESIAN_POINT('Ctrl Pts',(1.52141018960579,-1.73818913214068,1.77923201513049));
#19576=CARTESIAN_POINT('Ctrl Pts',(2.28528521654291,0.33684073493038,1.89043401607615));
#19577=CARTESIAN_POINT('Ctrl Pts',(0.955202501242366,2.1032303527304,2.0016360170218));
#19578=CARTESIAN_POINT('Ctrl Pts',(-1.25011163027303,1.94247547571461,2.11283801796746));
#19579=CARTESIAN_POINT('Ctrl Pts',(-2.30997543275355,0.00187206407255709,
2.22404001891312));
#19580=CARTESIAN_POINT('Ctrl Pts',(-1.25325848138969,-1.94044663051715,
2.33524201985877));
#19581=CARTESIAN_POINT('Ctrl Pts',(0.951792214663295,-2.10477589678604,
2.44644402080443));
#19582=CARTESIAN_POINT('Ctrl Pts',(2.28473620893343,-0.340544328114909,
2.55764602175008));
#19583=CARTESIAN_POINT('Ctrl Pts',(1.52422562126857,1.73572066664131,2.66884802269574));
#19584=CARTESIAN_POINT('Ctrl Pts',(-0.632900072980707,2.22158220235165,
2.7800500236414));
#19585=CARTESIAN_POINT('Ctrl Pts',(-2.21011306248986,0.671855812678093,
2.89125202458705));
#19586=CARTESIAN_POINT('Ctrl Pts',(-1.76224705404392,-1.49347758664845,
3.00245402553271));
#19587=CARTESIAN_POINT('Ctrl Pts',(0.300327974436209,-2.29036964049042,
3.11365602647836));
#19588=CARTESIAN_POINT('Ctrl Pts',(2.08771894852425,-0.988645322604533,
3.22485802742402));
#19589=CARTESIAN_POINT('Ctrl Pts',(1.96217801545981,1.21895341072497,3.33606002836968));
#19590=CARTESIAN_POINT('Ctrl Pts',(0.0387356283803547,2.30965138778668,
3.44726202931533));
#19591=CARTESIAN_POINT('Ctrl Pts',(-1.92019938070783,1.2840655436069,3.55846403026099));
#19592=CARTESIAN_POINT('Ctrl Pts',(-2.11969705463056,-0.918081901867433,
3.66966603120664));
#19593=CARTESIAN_POINT('Ctrl Pts',(-0.37696197157843,-2.27901067438232,
3.7808680321523));
#19594=CARTESIAN_POINT('Ctrl Pts',(1.71117524700055,-1.55173105144146,3.89207003309796));
#19595=CARTESIAN_POINT('Ctrl Pts',(2.23139944216054,0.597366312643301,4.00327203404361));
#19596=CARTESIAN_POINT('Ctrl Pts',(0.707040388502159,2.19910979057086,4.11447403498927));
#19597=CARTESIAN_POINT('Ctrl Pts',(-1.46516454485713,1.78585633197353,4.22567603593493));
#19598=CARTESIAN_POINT('Ctrl Pts',(-2.29487076257717,-0.263738819715705,
4.33687803688058));
#19599=CARTESIAN_POINT('Ctrl Pts',(-1.0218363276302,-2.07167577132429,4.44808003782624));
#19600=CARTESIAN_POINT('Ctrl Pts',(1.18748472594413,-1.98138083356179,4.55928203877189));
#19601=CARTESIAN_POINT('Ctrl Pts',(2.30873910126252,-0.0755893131216698,
4.67048403971755));
#19602=CARTESIAN_POINT('Ctrl Pts',(1.31454556387366,1.89946306688411,4.78168604066321));
#19603=CARTESIAN_POINT('Ctrl Pts',(-0.884137760920989,2.13407834946853,
4.89288804160886));
#19604=CARTESIAN_POINT('Ctrl Pts',(-2.27270469800289,0.413283604359384,
5.00409004255452));
#19605=CARTESIAN_POINT('Ctrl Pts',(-1.57884126997291,-1.68619400609389,
5.11529204350018));
#19606=CARTESIAN_POINT('Ctrl Pts',(0.561680408542726,-2.24064836612444,
5.22649404444582));
#19607=CARTESIAN_POINT('Ctrl Pts',(2.18754642622144,-0.74204488751176,5.33769604539148));
#19608=CARTESIAN_POINT('Ctrl Pts',(1.80901076907701,1.4364783393145,5.44889804633715));
#19609=CARTESIAN_POINT('Ctrl Pts',(-0.227082493175914,2.29878740279542,
5.56010004728278));
#19610=CARTESIAN_POINT('Ctrl Pts',(-2.0551049578498,1.05476708053322,5.67130204822846));
#19611=CARTESIAN_POINT('Ctrl Pts',(-2.00007901263631,-1.15571359997482,
5.7825040491741));
#19612=CARTESIAN_POINT('Ctrl Pts',(-0.112423745981393,-2.30723880066723,
5.89370605011977));
#19613=CARTESIAN_POINT('Ctrl Pts',(1.87824297772521,-1.34469078176803,6.00490805106541));
#19614=CARTESIAN_POINT('Ctrl Pts',(2.14791611466854,0.849968438411925,6.11611005201108));
#19615=CARTESIAN_POINT('Ctrl Pts',(0.449499977701421,2.26581988517564,6.22731205295673));
#19616=CARTESIAN_POINT('Ctrl Pts',(-1.66078330746703,1.60554937249238,6.33851405390239));
#19617=CARTESIAN_POINT('Ctrl Pts',(-2.24932661807747,-0.525851449692036,
6.44971605484804));
#19618=CARTESIAN_POINT('Ctrl Pts',(-0.776860394673336,-2.17542591450436,
6.5609180557937));
#19619=CARTESIAN_POINT('Ctrl Pts',(1.40742627626055,-1.83170446802946,6.67212005673936));
#19620=CARTESIAN_POINT('Ctrl Pts',(2.302118563571,0.190368330558053,6.783322057685));
#19621=CARTESIAN_POINT('Ctrl Pts',(1.08742919413144,2.0380107291021,6.89452405863067));
#19622=CARTESIAN_POINT('Ctrl Pts',(-1.1236481245081,2.01826778932498,7.00572605957632));
#19623=CARTESIAN_POINT('Ctrl Pts',(-2.30515086836339,0.149229547698346,
7.11692806052198));
#19624=CARTESIAN_POINT('Ctrl Pts',(-1.3744935190946,-1.85654452183408,7.22813006146763));
#19625=CARTESIAN_POINT('Ctrl Pts',(0.815582635998072,-2.16120681817335,
7.33933206241329));
#19626=CARTESIAN_POINT('Ctrl Pts',(2.25835799120458,-0.485601882318497,
7.45053406335894));
#19627=CARTESIAN_POINT('Ctrl Pts',(1.6318485532541,1.63494965094926,7.5617360643046));
#19628=CARTESIAN_POINT('Ctrl Pts',(-0.489888554829468,2.25743193449398,
7.67293806525026));
#19629=CARTESIAN_POINT('Ctrl Pts',(-2.16275135489337,0.811478144231195,
7.78414006619591));
#19630=CARTESIAN_POINT('Ctrl Pts',(-1.85393162516556,-1.37801594814403,
7.89534206714158));
#19631=CARTESIAN_POINT('Ctrl Pts',(0.153605637297925,-2.30486302861764,
8.00654406808722));
#19632=CARTESIAN_POINT('Ctrl Pts',(2.02039752512168,-1.11981505029068,8.11774606903289));
#19633=CARTESIAN_POINT('Ctrl Pts',(2.03594236675928,1.09129780058451,8.22894806997853));
#19634=CARTESIAN_POINT('Ctrl Pts',(0.185997657197281,2.30247329506172,8.3401500709242));
#19635=CARTESIAN_POINT('Ctrl Pts',(-1.83437382173052,1.40395102475339,8.45135207186985));
#19636=CARTESIAN_POINT('Ctrl Pts',(-2.17394593966066,-0.78099832785218,
8.56255407281551));
#19637=CARTESIAN_POINT('Ctrl Pts',(-0.521582285547066,-2.25030336416427,
8.67375607376116));
#19638=CARTESIAN_POINT('Ctrl Pts',(1.60870373387123,-1.65776554213267,8.78495807470682));
#19639=CARTESIAN_POINT('Ctrl Pts',(2.26495440895447,0.453864546487703,8.89616007565248));
#19640=CARTESIAN_POINT('Ctrl Pts',(0.845904254064056,2.14940472642079,9.00736207659812));
#19641=CARTESIAN_POINT('Ctrl Pts',(-1.34828328575767,1.87591753539018,9.11856407754379));
#19642=CARTESIAN_POINT('Ctrl Pts',(-2.30696595595385,-0.117243980915191,
9.22976607848944));
#19643=CARTESIAN_POINT('Ctrl Pts',(-1.1520193361947,-2.00142838810143,9.34096807943509));
#19644=CARTESIAN_POINT('Ctrl Pts',(1.05886536864935,-2.05472750787074,9.45217008038076));
#19645=CARTESIAN_POINT('Ctrl Pts',(2.29884885371374,-0.219384952913903,
9.5633720813264));
#19646=CARTESIAN_POINT('Ctrl Pts',(1.72210392161884,1.12922021260653,9.63750674862351));
#19647=CARTESIAN_POINT('Ctrl Pts',(1.21220412664425,1.53253944658748,9.67457408227206));
#19648=CARTESIAN_POINT('Ctrl Pts',(-1.95199070173634,-0.00143915622514865,
8.52413030787577));
#19649=CARTESIAN_POINT('Ctrl Pts',(-1.95352332736863,-0.226597580633425,
8.53693822952235));
#19650=CARTESIAN_POINT('Ctrl Pts',(-1.91755839154915,-0.451281101938663,
8.54974615116893));
#19651=CARTESIAN_POINT('Ctrl Pts',(-1.84195664432004,-0.661724275136593,
8.56255407281551));
#19652=CARTESIAN_POINT('Ctrl Pts',(-1.62315805495613,-1.27076667328954,
8.59962140646406));
#19653=CARTESIAN_POINT('Ctrl Pts',(-1.0723701702516,-1.76053501872691,8.63668874011261));
#19654=CARTESIAN_POINT('Ctrl Pts',(-0.441928557996276,-1.90666288777366,
8.67375607376116));
#19655=CARTESIAN_POINT('Ctrl Pts',(0.188513054259035,-2.0527907568204,8.71082340740971));
#19656=CARTESIAN_POINT('Ctrl Pts',(0.898608394065125,-1.85527814947654,
8.74789074105826));
#19657=CARTESIAN_POINT('Ctrl Pts',(1.36303117648205,-1.40458349770121,8.78495807470682));
#19658=CARTESIAN_POINT('Ctrl Pts',(1.82745395889897,-0.95388884592588,8.82202540835537));
#19659=CARTESIAN_POINT('Ctrl Pts',(2.04620418392672,-0.250012149719083,
8.85909274200392));
#19660=CARTESIAN_POINT('Ctrl Pts',(1.91907093729219,0.384516228373164,8.89616007565247));
#19661=CARTESIAN_POINT('Ctrl Pts',(1.79193769065766,1.01904460646541,8.93322740930103));
#19662=CARTESIAN_POINT('Ctrl Pts',(1.31892097236085,1.58422466644311,8.97029474294957));
#19663=CARTESIAN_POINT('Ctrl Pts',(0.716714689908818,1.82123349792685,9.00736207659813));
#19664=CARTESIAN_POINT('Ctrl Pts',(0.507473848776133,1.90358389628803,9.02024138439875));
#19665=CARTESIAN_POINT('Ctrl Pts',(0.282636413049304,1.9463153545146,9.03312069219937));
#19666=CARTESIAN_POINT('Ctrl Pts',(0.0562592026297114,1.95117115182352,
9.046));
#19667=CARTESIAN_POINT('Ctrl Pts',(-0.905550660636153,-1.26792405592273,
1.45716771982052E-16));
#19668=CARTESIAN_POINT('Ctrl Pts',(-0.937331646933896,-1.25093119319315,
1.27175061552484E-16));
#19669=CARTESIAN_POINT('Ctrl Pts',(-0.968423391396878,-1.23278887404085,
4.27877505352727E-17));
#19670=CARTESIAN_POINT('Ctrl Pts',(-0.998756220109605,-1.21351103938415,
8.67361737988404E-19));
#19671=CARTESIAN_POINT('Ctrl Pts',(-1.04879905844205,-1.1817066345836,-4.27343170489691E-17));
#19672=CARTESIAN_POINT('Ctrl Pts',(-1.09677754676758,-1.14681449344115,
3.59228313652207E-16));
#19673=CARTESIAN_POINT('Ctrl Pts',(-1.14261320333336,-1.1091553561269,4.82253126321552E-16));
#19674=CARTESIAN_POINT('Ctrl Pts',(-1.16875585300247,-1.08767623468714,
5.52421087668592E-16));
#19675=CARTESIAN_POINT('Ctrl Pts',(-1.19420116520872,-1.06529603829454,
1.68485755535521E-16));
#19676=CARTESIAN_POINT('Ctrl Pts',(-1.21893184621838,-1.04206746474762,
1.70002900645727E-16));
#19677=CARTESIAN_POINT('Ctrl Pts',(-1.23255995383574,-1.02926710959479,
1.70838939767535E-16));
#19678=CARTESIAN_POINT('Ctrl Pts',(-1.24597488110422,-1.01620487704946,
4.21475736447755E-16));
#19679=CARTESIAN_POINT('Ctrl Pts',(-1.25915060380592,-1.0029128321029,4.02455846426619E-16));
#19680=CARTESIAN_POINT('Ctrl Pts',(-1.30303064134819,-0.95864539839369,
3.39112566739263E-16));
#19681=CARTESIAN_POINT('Ctrl Pts',(-1.34430260426558,-0.91179514360288,
3.08161369943384E-16));
#19682=CARTESIAN_POINT('Ctrl Pts',(-1.38287779953103,-0.862711096565261,
2.84494650060196E-16));
#19683=CARTESIAN_POINT('Ctrl Pts',(-1.41251185733787,-0.825003977332371,
2.66313512147855E-16));
#19684=CARTESIAN_POINT('Ctrl Pts',(-1.44055413744545,-0.785977345707785,
2.85602281713357E-16));
#19685=CARTESIAN_POINT('Ctrl Pts',(-1.46695437986393,-0.745771217825177,
2.63677968348475E-16));
#19686=CARTESIAN_POINT('Ctrl Pts',(-1.48000187887279,-0.725900589162651,
2.52842558113835E-16));
#19687=CARTESIAN_POINT('Ctrl Pts',(-1.49264815413029,-0.705741645745626,
3.81368532133475E-16));
#19688=CARTESIAN_POINT('Ctrl Pts',(-1.50488615061787,-0.685310125526541,
3.53883589099269E-16));
#19689=CARTESIAN_POINT('Ctrl Pts',(-1.51114001186157,-0.674869209599035,
3.398382328842E-16));
#19690=CARTESIAN_POINT('Ctrl Pts',(-1.51728238793534,-0.664365181000008,
3.54964001115812E-16));
#19691=CARTESIAN_POINT('Ctrl Pts',(-1.52331182355158,-0.653802123157991,
3.53883589099269E-16));
#19692=CARTESIAN_POINT('Ctrl Pts',(-1.55543280121804,-0.597528905127582,
3.48127844704137E-16));
#19693=CARTESIAN_POINT('Ctrl Pts',(-1.5843593035114,-0.539569562213937,
2.67786881775446E-16));
#19694=CARTESIAN_POINT('Ctrl Pts',(-1.60999744801157,-0.480277394578745,
2.4980018054066E-16));
#19695=CARTESIAN_POINT('Ctrl Pts',(-1.6361318010197,-0.419837668155283,
2.31465359176401E-16));
#19696=CARTESIAN_POINT('Ctrl Pts',(-1.65885002952378,-0.358012230099105,
4.67501104767292E-16));
#19697=CARTESIAN_POINT('Ctrl Pts',(-1.67801828739638,-0.295134384099341,
4.57966997657877E-16));
#19698=CARTESIAN_POINT('Ctrl Pts',(-1.69037417655557,-0.254603225717345,
4.51821297226535E-16));
#19699=CARTESIAN_POINT('Ctrl Pts',(-1.70125428685937,-0.213633977893128,
1.06733149524263E-17));
#19700=CARTESIAN_POINT('Ctrl Pts',(-1.71061315113863,-0.172309644008052,
-5.55111512312578E-17));
#19701=CARTESIAN_POINT('Ctrl Pts',(-1.71583359551538,-0.149258622001936,
-9.24293406618695E-17));
#19702=CARTESIAN_POINT('Ctrl Pts',(-1.7205805610286,-0.126097041535353,
3.62932093827782E-16));
#19703=CARTESIAN_POINT('Ctrl Pts',(-1.72484497590278,-0.102838875523928,
3.60822483003176E-16));
#19704=CARTESIAN_POINT('Ctrl Pts',(-1.72698171347111,-0.0911850851322128,
3.59765436529865E-16));
#19705=CARTESIAN_POINT('Ctrl Pts',(-1.72899754888149,-0.0795054094991753,
1.33624776520754E-16));
#19706=CARTESIAN_POINT('Ctrl Pts',(-1.73089043201219,-0.0678066984905219,
1.38777878078145E-16));
#19707=CARTESIAN_POINT('Ctrl Pts',(-1.74172160283504,-0.000866095931865457,
1.68264179863231E-16));
#19708=CARTESIAN_POINT('Ctrl Pts',(-1.748486900033,0.0664195158076909,2.42458198468553E-16));
#19709=CARTESIAN_POINT('Ctrl Pts',(-1.75106690168969,0.133692207227197,
2.22044604925031E-16));
#19710=CARTESIAN_POINT('Ctrl Pts',(-1.75197579459359,0.157391289628443,
2.14853225699892E-16));
#19711=CARTESIAN_POINT('Ctrl Pts',(-1.7523649021625,0.181089059905603,-1.04868588637259E-16));
#19712=CARTESIAN_POINT('Ctrl Pts',(-1.75222770108741,0.204770690960275,
-9.71445146547012E-17));
#19713=CARTESIAN_POINT('Ctrl Pts',(-1.75185206838866,0.269606881041249,
-6.21195546873158E-17));
#19714=CARTESIAN_POINT('Ctrl Pts',(-1.74753527769623,0.334321428897923,
1.54729584489575E-16));
#19715=CARTESIAN_POINT('Ctrl Pts',(-1.73949435710187,0.398678851668467,
8.32667268468867E-17));
#19716=CARTESIAN_POINT('Ctrl Pts',(-1.7312762859938,0.46445414076046,1.02294621704162E-17));
#19717=CARTESIAN_POINT('Ctrl Pts',(-1.71916809095178,0.529857212284545,
-1.51627889474086E-16));
#19718=CARTESIAN_POINT('Ctrl Pts',(-1.70334767938921,0.594640505552203,
-1.66533453693773E-16));
#19719=CARTESIAN_POINT('Ctrl Pts',(-1.70064831213801,0.605694193983744,
-1.69076724566096E-16));
#19720=CARTESIAN_POINT('Ctrl Pts',(-1.69784071539616,0.616729589129694,
5.32060987810746E-16));
#19721=CARTESIAN_POINT('Ctrl Pts',(-1.69492950185833,0.627731892802461,
5.27355936696949E-16));
#19722=CARTESIAN_POINT('Ctrl Pts',(-1.67758049779776,0.693298711798846,
4.9931678744945E-16));
#19723=CARTESIAN_POINT('Ctrl Pts',(-1.65652692130866,0.757811857431264,
1.02969912804589E-16));
#19724=CARTESIAN_POINT('Ctrl Pts',(-1.63202614811433,0.82101547035702,8.32667268468867E-17));
#19725=CARTESIAN_POINT('Ctrl Pts',(-1.60700935125733,0.885550247796537,
6.31485617330762E-17));
#19726=CARTESIAN_POINT('Ctrl Pts',(-1.57839845257882,0.948720629503181,
8.44128967647446E-17));
#19727=CARTESIAN_POINT('Ctrl Pts',(-1.54641225600304,1.01025741355839,1.94289029309402E-16));
#19728=CARTESIAN_POINT('Ctrl Pts',(-1.51418344328006,1.07226095574858,3.04998575226134E-16));
#19729=CARTESIAN_POINT('Ctrl Pts',(-1.47852761223994,1.13260700774386,2.72099366666861E-16));
#19730=CARTESIAN_POINT('Ctrl Pts',(-1.43961707028964,1.19100921034501,4.16333634234434E-16));
#19731=CARTESIAN_POINT('Ctrl Pts',(-1.42987064738873,1.20563795968555,4.52461842633911E-16));
#19732=CARTESIAN_POINT('Ctrl Pts',(-1.41991978147756,1.22014465371079,-1.08678851106874E-16));
#19733=CARTESIAN_POINT('Ctrl Pts',(-1.40976671738967,1.23452457045435,-1.11022302462516E-16));
#19734=CARTESIAN_POINT('Ctrl Pts',(-1.40175176458173,1.24587625237856,-1.12872251587291E-16));
#19735=CARTESIAN_POINT('Ctrl Pts',(-1.39360965291877,1.25715028749333,2.28365264434682E-16));
#19736=CARTESIAN_POINT('Ctrl Pts',(-1.38535473796849,1.2683268547918,2.22044604925031E-16));
#19737=CARTESIAN_POINT('Ctrl Pts',(-1.34246203780014,1.32640051792846,1.89202334005651E-16));
#19738=CARTESIAN_POINT('Ctrl Pts',(-1.2964535599336,1.38195119811813,-1.79031912722901E-17));
#19739=CARTESIAN_POINT('Ctrl Pts',(-1.24757009345088,1.43469804908261,2.77555756156289E-17));
#19740=CARTESIAN_POINT('Ctrl Pts',(-1.19857852782046,1.48756154254492,7.35153106660103E-17));
#19741=CARTESIAN_POINT('Ctrl Pts',(-1.14669881160737,1.53760980197427,-1.09074190413862E-16));
#19742=CARTESIAN_POINT('Ctrl Pts',(-1.09212377872999,1.58454380591305,-1.38777878078145E-16));
#19743=CARTESIAN_POINT('Ctrl Pts',(-1.03871943285682,1.63047103027572,-1.67844393041064E-16));
#19744=CARTESIAN_POINT('Ctrl Pts',(-0.982733594885126,1.67341702936247,
5.10578859420299E-17));
#19745=CARTESIAN_POINT('Ctrl Pts',(-0.924307244265998,1.71307238365465,
8.32667268468867E-17));
#19746=CARTESIAN_POINT('Ctrl Pts',(-0.90368282336986,1.72707066882976,9.4636403103562E-17));
#19747=CARTESIAN_POINT('Ctrl Pts',(-0.882753967690277,1.74065858283188,
-3.60501930089703E-18));
#19748=CARTESIAN_POINT('Ctrl Pts',(-0.861525859670525,1.75382131162755,
0.));
#19749=CARTESIAN_POINT('Origin',(0.,0.,0.));
#19750=CARTESIAN_POINT('Origin',(-0.866025403784439,-1.5,-4.));
#19751=CARTESIAN_POINT('',(-0.866025403784439,-1.5,-4.));
#19752=CARTESIAN_POINT('',(0.866025403784439,-1.5,-4.));
#19753=CARTESIAN_POINT('',(-0.43301270189222,-1.5,-4.));
#19754=CARTESIAN_POINT('',(-0.866025403784439,-1.5,-2.));
#19755=CARTESIAN_POINT('',(-0.866025403784439,-1.5,-4.));
#19756=CARTESIAN_POINT('',(0.866025403784439,-1.5,-2.));
#19757=CARTESIAN_POINT('',(-0.866025403784439,-1.5,-2.));
#19758=CARTESIAN_POINT('',(0.866025403784439,-1.5,-4.));
#19759=CARTESIAN_POINT('Origin',(-1.73205080756888,2.12115047744981E-16,
-4.));
#19760=CARTESIAN_POINT('',(-1.73205080756888,2.12115047744981E-16,-4.));
#19761=CARTESIAN_POINT('',(-1.51554445662277,-0.375,-4.));
#19762=CARTESIAN_POINT('',(-1.73205080756888,2.77555756156289E-16,-2.));
#19763=CARTESIAN_POINT('',(-1.73205080756888,2.12115047744981E-16,-4.));
#19764=CARTESIAN_POINT('',(-1.73205080756888,2.12115047744981E-16,-2.));
#19765=CARTESIAN_POINT('Origin',(-0.866025403784438,1.5,-4.));
#19766=CARTESIAN_POINT('',(-0.866025403784438,1.5,-4.));
#19767=CARTESIAN_POINT('',(-1.08253175473055,1.125,-4.));
#19768=CARTESIAN_POINT('',(-0.866025403784438,1.5,-2.));
#19769=CARTESIAN_POINT('',(-0.866025403784438,1.5,-4.));
#19770=CARTESIAN_POINT('',(-0.866025403784438,1.5,-2.));
#19771=CARTESIAN_POINT('Origin',(0.866025403784439,1.5,-4.));
#19772=CARTESIAN_POINT('',(0.866025403784439,1.5,-4.));
#19773=CARTESIAN_POINT('',(0.43301270189222,1.5,-4.));
#19774=CARTESIAN_POINT('',(0.866025403784439,1.5,-2.));
#19775=CARTESIAN_POINT('',(0.866025403784439,1.5,-4.));
#19776=CARTESIAN_POINT('',(0.866025403784439,1.5,-2.));
#19777=CARTESIAN_POINT('Origin',(1.73205080756888,0.,-4.));
#19778=CARTESIAN_POINT('',(1.73205080756888,0.,-4.));
#19779=CARTESIAN_POINT('',(1.51554445662277,0.375,-4.));
#19780=CARTESIAN_POINT('',(1.73205080756888,0.,-2.));
#19781=CARTESIAN_POINT('',(1.73205080756888,0.,-4.));
#19782=CARTESIAN_POINT('',(1.73205080756888,0.,-2.));
#19783=CARTESIAN_POINT('Origin',(0.866025403784439,-1.5,-4.));
#19784=CARTESIAN_POINT('',(1.08253175473055,-1.125,-4.));
#19785=CARTESIAN_POINT('',(0.866025403784439,-1.5,-2.));
#19786=CARTESIAN_POINT('Origin',(0.,2.77555756156289E-16,-2.));
#19787=CARTESIAN_POINT('Origin',(0.,0.,0.));
#19788=CARTESIAN_POINT('',(-3.5,-4.28626379701574E-16,0.));
#19789=CARTESIAN_POINT('Origin',(0.,0.,0.));
#19790=CARTESIAN_POINT('Origin',(0.,0.,-4.));
#19791=CARTESIAN_POINT('',(-3.5,-4.28626379701574E-16,-4.));
#19792=CARTESIAN_POINT('',(-3.5,-4.28626379701574E-16,-4.));
#19793=CARTESIAN_POINT('Origin',(0.,0.,-4.));
#19794=CARTESIAN_POINT('Origin',(0.,0.,-4.));
#19795=CARTESIAN_POINT('Origin',(0.,0.,10.));
#19841=UNCERTAINTY_MEASURE_WITH_UNIT(LENGTH_MEASURE(0.01),#19864,
'DISTANCE_ACCURACY_VALUE',
'Maximum model space distance between geometric entities at asserted c
onnectivities');
#19842=UNCERTAINTY_MEASURE_WITH_UNIT(LENGTH_MEASURE(0.01),#19864,
'DISTANCE_ACCURACY_VALUE',
'Maximum model space distance between geometric entities at asserted c
onnectivities');
#19862=(
GEOMETRIC_REPRESENTATION_CONTEXT(3)
GLOBAL_UNCERTAINTY_ASSIGNED_CONTEXT((#19841))
GLOBAL_UNIT_ASSIGNED_CONTEXT((#19864,#19866,#19867))
REPRESENTATION_CONTEXT('','3D')
);
#19863=(
GEOMETRIC_REPRESENTATION_CONTEXT(3)
GLOBAL_UNCERTAINTY_ASSIGNED_CONTEXT((#19842))
GLOBAL_UNIT_ASSIGNED_CONTEXT((#19864,#19866,#19867))
REPRESENTATION_CONTEXT('','3D')
);
#19864=(
LENGTH_UNIT()
NAMED_UNIT(*)
SI_UNIT(.MILLI.,.METRE.)
);
#19866=(
NAMED_UNIT(*)
PLANE_ANGLE_UNIT()
SI_UNIT($,.RADIAN.)
);
#19867=(
NAMED_UNIT(*)
SI_UNIT($,.STERADIAN.)
SOLID_ANGLE_UNIT()
);
#19887=SHAPE_DEFINITION_REPRESENTATION(#19907,#19953);
#19907=PRODUCT_DEFINITION_SHAPE('',$,#19974);
#19953=SHAPE_REPRESENTATION('',(#7117),#19862);
#19954=PRODUCT_DEFINITION_CONTEXT('part definition',#20016,'design');
#19974=PRODUCT_DEFINITION('Socket head cap screw M4x10',
'Socket head cap screw M4x10',#19994,#19954);
#19994=PRODUCT_DEFINITION_FORMATION('',$,#20037);
#20016=APPLICATION_CONTEXT(
'Core Data for Automotive Mechanical Design Process');
#20017=PRODUCT_CONTEXT('part definition',#20016,'mechanical');
#20037=PRODUCT('Socket head cap screw M4x10',
'Socket head cap screw M4x10',$,(#20017));
#20044=PRESENTATION_STYLE_ASSIGNMENT((#20051));
#20051=SURFACE_STYLE_USAGE(.BOTH.,#20058);
#20058=SURFACE_SIDE_STYLE('',(#20065));
#20065=SURFACE_STYLE_FILL_AREA(#20072);
#20072=FILL_AREA_STYLE('Dark gray',(#20079));
#20079=FILL_AREA_STYLE_COLOUR('Dark gray',#20086);
#20086=COLOUR_RGB('Dark gray',0.250980392156863,0.282352941176471,0.32156862745098);
ENDSEC;
END-ISO-10303-21;
